ISO-10303-21;
HEADER;
FILE_DESCRIPTION (('STEP AP214'),
    '1' );
FILE_NAME ('top housing_top housing.step',
    '2026-10-08T15:02:10',
    ( '' ),
    ( '' ),
    'SwSTEP 2.0',
    'SolidWorks 2026',
    '' );
FILE_SCHEMA (( 'AUTOMOTIVE_DESIGN' ));
ENDSEC;

DATA;
#16=CARTESIAN_POINT ( 'NONE',  ( 2.465190328815661892E-29, 24.63401512838760610, -77.51594804401857175 ) ) ;
#21=ADVANCED_FACE ( 'NONE', ( #14586 ), #5680, .F. ) ;
#39=DIRECTION ( 'NONE',  ( -1.000000000000000000, 0.000000000000000000, 0.000000000000000000 ) ) ;
#79=PRODUCT_DEFINITION_SHAPE ( 'NONE', 'NONE',  #8374 ) ;
#84=DIRECTION ( 'NONE',  ( 0.000000000000000000, 1.000000000000000000, 0.000000000000000000 ) ) ;
#95=ORIENTED_EDGE ( 'NONE', *, *, #2038, .F. ) ;
#99=ORIENTED_EDGE ( 'NONE', *, *, #17132, .T. ) ;
#108=AXIS2_PLACEMENT_3D ( 'NONE', #21877, #21538, #9854 ) ;
#131=AXIS2_PLACEMENT_3D ( 'NONE', #8453, #22168, #4530 ) ;
#145=FACE_OUTER_BOUND ( 'NONE', #18733, .T. ) ;
#153=CARTESIAN_POINT ( 'NONE',  ( 1.387778780781446180E-13, -19.80000000000006111, 78.50000000000000000 ) ) ;
#169=AXIS2_PLACEMENT_3D ( 'NONE', #2504, #9798, #9382 ) ;
#179=ORIENTED_EDGE ( 'NONE', *, *, #598, .F. ) ;
#185=ORIENTED_EDGE ( 'NONE', *, *, #19709, .T. ) ;
#197=CARTESIAN_POINT ( 'NONE',  ( 0.000000000000000000, 0.000000000000000000, 78.50000000000000000 ) ) ;
#198=EDGE_CURVE ( 'NONE', #16686, #4564, #9428, .T. ) ;
#203=CARTESIAN_POINT ( 'NONE',  ( -22.92002576459826102, 9.983672621040497575, 0.6612741795047580862 ) ) ;
#210=ORIENTED_EDGE ( 'NONE', *, *, #8940, .F. ) ;
#223=VECTOR ( 'NONE', #786, 1000.000000000000000 ) ;
#239=CIRCLE ( 'NONE', #21420, 3.000000000000002665 ) ;
#246=FACE_OUTER_BOUND ( 'NONE', #1813, .T. ) ;
#253=EDGE_LOOP ( 'NONE', ( #21985, #19311, #21733, #15919, #6601, #3460 ) ) ;
#278=ORIENTED_EDGE ( 'NONE', *, *, #1896, .T. ) ;
#281=ORIENTED_EDGE ( 'NONE', *, *, #14770, .F. ) ;
#316=CARTESIAN_POINT ( 'NONE',  ( -24.43175472503111223, 5.307112681608126437, 8.481714195412854096 ) ) ;
#320=CARTESIAN_POINT ( 'NONE',  ( 0.000000000000000000, -23.00000000000006040, 75.00000000000000000 ) ) ;
#324=VERTEX_POINT ( 'NONE', #21527 ) ;
#336=AXIS2_PLACEMENT_3D ( 'NONE', #20789, #15968, #7308 ) ;
#343=DIRECTION ( 'NONE',  ( -1.000000000000000000, 0.000000000000000000, 0.000000000000000000 ) ) ;
#351=VERTEX_POINT ( 'NONE', #11636 ) ;
#418=CARTESIAN_POINT ( 'NONE',  ( -22.24589463867734906, 5.847797018635430888, 8.118367508314726422 ) ) ;
#422=CARTESIAN_POINT ( 'NONE',  ( 1.526556658859590748E-13, -21.00000000000006395, -75.00000000000000000 ) ) ;
#425=CARTESIAN_POINT ( 'NONE',  ( -21.00000000000000000, 0.000000000000000000, 75.00000000000000000 ) ) ;
#440=EDGE_CURVE ( 'NONE', #17900, #18699, #12299, .T. ) ;
#442=CIRCLE ( 'NONE', #19821, 21.63401512838748175 ) ;
#448=LINE ( 'NONE', #14302, #21639 ) ;
#478=CARTESIAN_POINT ( 'NONE',  ( 0.000000000000000000, 0.000000000000000000, 69.99999999999998579 ) ) ;
#485=EDGE_CURVE ( 'NONE', #10116, #8679, #18757, .T. ) ;
#510=ORIENTED_EDGE ( 'NONE', *, *, #7205, .T. ) ;
#526=LINE ( 'NONE', #7615, #8756 ) ;
#536=EDGE_LOOP ( 'NONE', ( #20404, #210, #5432, #5454, #20475, #13502 ) ) ;
#542=CARTESIAN_POINT ( 'NONE',  ( 1.665334536937735820E-13, -23.00000000000006040, 69.99999999999998579 ) ) ;
#564=ORIENTED_EDGE ( 'NONE', *, *, #4047, .T. ) ;
#574=DIRECTION ( 'NONE',  ( -1.000000000000000000, 0.000000000000000000, 0.000000000000000000 ) ) ;
#580=VERTEX_POINT ( 'NONE', #8267 ) ;
#585=CARTESIAN_POINT ( 'NONE',  ( 0.000000000000000000, 0.000000000000000000, 75.00000000000000000 ) ) ;
#588=DIRECTION ( 'NONE',  ( 0.000000000000000000, 0.000000000000000000, -1.000000000000000000 ) ) ;
#598=EDGE_CURVE ( 'NONE', #15940, #3862, #788, .T. ) ;
#604=ORIENTED_EDGE ( 'NONE', *, *, #18360, .F. ) ;
#623=EDGE_LOOP ( 'NONE', ( #16790, #6594, #15513, #3933, #16241, #20562 ) ) ;
#635=DIRECTION ( 'NONE',  ( -0.000000000000000000, -1.000000000000000000, -0.000000000000000000 ) ) ;
#636=CARTESIAN_POINT ( 'NONE',  ( -21.73616590321354280, 7.534719468122247577, -6.606834546510540029 ) ) ;
#645=VERTEX_POINT ( 'NONE', #952 ) ;
#651=ORIENTED_EDGE ( 'NONE', *, *, #13199, .F. ) ;
#693=CARTESIAN_POINT ( 'NONE',  ( -22.63401512838757057, 0.000000000000000000, -77.51594804401857175 ) ) ;
#717=CARTESIAN_POINT ( 'NONE',  ( 0.000000000000000000, 0.000000000000000000, -77.51594804401857175 ) ) ;
#727=CARTESIAN_POINT ( 'NONE',  ( -22.63401512838757057, 0.000000000000000000, 77.51594804401857175 ) ) ;
#736=ORIENTED_EDGE ( 'NONE', *, *, #485, .T. ) ;
#758=VERTEX_POINT ( 'NONE', #15024 ) ;
#763=FACE_OUTER_BOUND ( 'NONE', #5768, .T. ) ;
#786=DIRECTION ( 'NONE',  ( -0.000000000000000000, 0.000000000000000000, -1.000000000000000000 ) ) ;
#788=CIRCLE ( 'NONE', #14454, 19.63401512838747820 ) ;
#794=ORIENTED_EDGE ( 'NONE', *, *, #11036, .F. ) ;
#812=AXIS2_PLACEMENT_3D ( 'NONE', #10619, #3959, #20954 ) ;
#830=ORIENTED_EDGE ( 'NONE', *, *, #2939, .T. ) ;
#831=AXIS2_PLACEMENT_3D ( 'NONE', #5353, #20662, #13482 ) ;
#836=DIRECTION ( 'NONE',  ( 0.000000000000000000, 0.000000000000000000, -1.000000000000000000 ) ) ;
#837=ORIENTED_EDGE ( 'NONE', *, *, #13199, .T. ) ;
#844=CIRCLE ( 'NONE', #13436, 21.00000000000008171 ) ;
#850=CARTESIAN_POINT ( 'NONE',  ( -24.24755750141337174, -6.112543499224761590, 7.941049042234675781 ) ) ;
#868=ORIENTED_EDGE ( 'NONE', *, *, #19516, .F. ) ;
#872=VECTOR ( 'NONE', #84, 1000.000000000000000 ) ;
#883=CARTESIAN_POINT ( 'NONE',  ( 1.665334536937735568E-13, -23.00000000000006395, 75.00000000000000000 ) ) ;
#884=CIRCLE ( 'NONE', #1615, 21.00000000000008527 ) ;
#914=DIRECTION ( 'NONE',  ( -1.000000000000000000, 0.000000000000000000, 0.000000000000000000 ) ) ;
#925=EDGE_CURVE ( 'NONE', #4211, #12391, #16929, .T. ) ;
#929=VECTOR ( 'NONE', #5748, 1000.000000000000000 ) ;
#950=AXIS2_PLACEMENT_3D ( 'NONE', #2433, #2106, #17539 ) ;
#952=CARTESIAN_POINT ( 'NONE',  ( 0.000000000000000000, 21.00000000000006395, -75.00000000000000000 ) ) ;
#964=CARTESIAN_POINT ( 'NONE',  ( -24.94801726869080483, -1.644149540150739774, 9.869507958217397459 ) ) ;
#965=CARTESIAN_POINT ( 'NONE',  ( -20.71238021041400756, 9.999865301160326680, 0.3337829719016462415 ) ) ;
#973=DIRECTION ( 'NONE',  ( -1.000000000000000000, 0.000000000000000000, 0.000000000000000000 ) ) ;
#983=EDGE_CURVE ( 'NONE', #1365, #10566, #7340, .T. ) ;
#987=DIRECTION ( 'NONE',  ( 0.000000000000000000, 0.000000000000000000, -1.000000000000000000 ) ) ;
#992=DIRECTION ( 'NONE',  ( 1.000000000000000000, 0.000000000000000000, 0.000000000000000000 ) ) ;
#994=LINE ( 'NONE', #19555, #3715 ) ;
#998=CYLINDRICAL_SURFACE ( 'NONE', #19140, 23.00000000000008882 ) ;
#1031=AXIS2_PLACEMENT_3D ( 'NONE', #727, #2413, #7826 ) ;
#1033=ADVANCED_FACE ( 'NONE', ( #15252 ), #17682, .F. ) ;
#1035=FACE_OUTER_BOUND ( 'NONE', #14806, .T. ) ;
#1043=ORIENTED_EDGE ( 'NONE', *, *, #10914, .T. ) ;
#1050=CARTESIAN_POINT ( 'NONE',  ( 1.526556658859591000E-13, -22.63401512838754570, -77.51594804401857175 ) ) ;
#1071=CARTESIAN_POINT ( 'NONE',  ( -23.33371624899309893, -8.978322754191188082, -4.451123584478842155 ) ) ;
#1082=ORIENTED_EDGE ( 'NONE', *, *, #11545, .T. ) ;
#1098=CARTESIAN_POINT ( 'NONE',  ( -24.94744066671306015, 1.651985823032437350, -9.868045913509542189 ) ) ;
#1104=CARTESIAN_POINT ( 'NONE',  ( -22.17508266256912819, -6.110112796411599767, -7.922854749118508622 ) ) ;
#1112=ORIENTED_EDGE ( 'NONE', *, *, #19320, .F. ) ;
#1114=FACE_OUTER_BOUND ( 'NONE', #21076, .T. ) ;
#1135=SHAPE_REPRESENTATION_RELATIONSHIP ( 'NONE' , 'NONE' ,  #14642, #20620 ) ;
#1150=EDGE_CURVE ( 'NONE', #18699, #10116, #5395, .T. ) ;
#1190=VECTOR ( 'NONE', #12712, 1000.000000000000000 ) ;
#1207=DIRECTION ( 'NONE',  ( -1.000000000000000000, 0.000000000000000000, 0.000000000000000000 ) ) ;
#1210=DIRECTION ( 'NONE',  ( 0.000000000000000000, 0.000000000000000000, 1.000000000000000000 ) ) ;
#1211=EDGE_CURVE ( 'NONE', #9851, #16873, #2253, .T. ) ;
#1214=CARTESIAN_POINT ( 'NONE',  ( -23.70785736019170997, 7.942585827099451379, -6.110416780456437991 ) ) ;
#1219=CARTESIAN_POINT ( 'NONE',  ( -22.17907062223998338, -6.115498295305363818, 7.938811080418386013 ) ) ;
#1228=AXIS2_PLACEMENT_3D ( 'NONE', #8171, #4772, #4997 ) ;
#1258=CARTESIAN_POINT ( 'NONE',  ( 0.000000000000000000, -23.00000000000006040, -55.00000000000000000 ) ) ;
#1271=AXIS2_PLACEMENT_3D ( 'NONE', #9116, #20803, #5381 ) ;
#1296=CARTESIAN_POINT ( 'NONE',  ( -24.87076642133107995, -2.621478783564629378, 9.673133369187967290 ) ) ;
#1328=FACE_OUTER_BOUND ( 'NONE', #7121, .T. ) ;
#1331=CARTESIAN_POINT ( 'NONE',  ( -22.56784948551151615, -4.447299220502048733, 8.962591915120089681 ) ) ;
#1365=VERTEX_POINT ( 'NONE', #2034 ) ;
#1384=CARTESIAN_POINT ( 'NONE',  ( 1.526556658859591000E-13, -22.63401512838754570, 77.51594804401857175 ) ) ;
#1426=DIRECTION ( 'NONE',  ( -2.162300680179986877E-16, -1.000000000000000000, 0.000000000000000000 ) ) ;
#1435=CARTESIAN_POINT ( 'NONE',  ( -25.00000000000013500, 6.609496070381316956E-17, -10.00000000000000000 ) ) ;
#1441=FACE_OUTER_BOUND ( 'NONE', #21298, .T. ) ;
#1442=CARTESIAN_POINT ( 'NONE',  ( 1.455845656607152363E-13, -21.63401512838760610, -77.51594804401857175 ) ) ;
#1474=ORIENTED_EDGE ( 'NONE', *, *, #16262, .T. ) ;
#1487=ORIENTED_EDGE ( 'NONE', *, *, #6538, .F. ) ;
#1504=CARTESIAN_POINT ( 'NONE',  ( -25.00000000000010303, 0.000000000000000000, 75.00000000000000000 ) ) ;
#1505=AXIS2_PLACEMENT_3D ( 'NONE', #2740, #9620, #3068 ) ;
#1512=CIRCLE ( 'NONE', #3297, 17.50000000000007816 ) ;
#1548=CIRCLE ( 'NONE', #4759, 21.63401512838748175 ) ;
#1555=CARTESIAN_POINT ( 'NONE',  ( -20.71254002826594842, -9.999534281261636792, -0.6688830150170183009 ) ) ;
#1567=AXIS2_PLACEMENT_3D ( 'NONE', #14727, #987, #14093 ) ;
#1582=CARTESIAN_POINT ( 'NONE',  ( 0.000000000000000000, 0.000000000000000000, 69.99999999999998579 ) ) ;
#1596=EDGE_CURVE ( 'NONE', #16287, #758, #10152, .T. ) ;
#1615=AXIS2_PLACEMENT_3D ( 'NONE', #17502, #2069, #8949 ) ;
#1644=VERTEX_POINT ( 'NONE', #11142 ) ;
#1664=CARTESIAN_POINT ( 'NONE',  ( 0.000000000000000000, 23.00000000000006040, 75.00000000000000000 ) ) ;
#1667=DIRECTION ( 'NONE',  ( -2.162300680179986877E-16, -1.000000000000000000, 0.000000000000000000 ) ) ;
#1668=CARTESIAN_POINT ( 'NONE',  ( -21.01325146862401638, -9.352110752727961440, -3.555790053721613830 ) ) ;
#1674=ADVANCED_FACE ( 'NONE', ( #1114 ), #14825, .T. ) ;
#1690=DIRECTION ( 'NONE',  ( 1.000000000000000000, 0.000000000000000000, 0.000000000000000000 ) ) ;
#1708=DIRECTION ( 'NONE',  ( -0.000000000000000000, 0.000000000000000000, -1.000000000000000000 ) ) ;
#1714=ORIENTED_EDGE ( 'NONE', *, *, #18092, .T. ) ;
#1722=EDGE_CURVE ( 'NONE', #12201, #9941, #15183, .T. ) ;
#1724=CARTESIAN_POINT ( 'NONE',  ( -17.50000000000000711, 0.000000000000000000, -55.00000000000000000 ) ) ;
#1737=AXIS2_PLACEMENT_3D ( 'NONE', #10092, #15720, #17402 ) ;
#1742=DIRECTION ( 'NONE',  ( 0.000000000000000000, 0.000000000000000000, 1.000000000000000000 ) ) ;
#1769=CARTESIAN_POINT ( 'NONE',  ( -22.38013505867163389, 5.310942760180386024, 8.479298789953642057 ) ) ;
#1773=CARTESIAN_POINT ( 'NONE',  ( -24.87078308609252630, 2.620408809423218077, 9.673169865297577275 ) ) ;
#1793=DIRECTION ( 'NONE',  ( -0.000000000000000000, 0.000000000000000000, -1.000000000000000000 ) ) ;
#1794=CARTESIAN_POINT ( 'NONE',  ( -23.00000000000000000, 0.000000000000000000, -60.00000000000000000 ) ) ;
#1801=EDGE_LOOP ( 'NONE', ( #4632, #13971, #7716, #8469 ) ) ;
#1813=EDGE_LOOP ( 'NONE', ( #16398, #4768, #9072, #7529 ) ) ;
#1838=VERTEX_POINT ( 'NONE', #18450 ) ;
#1844=ORIENTED_EDGE ( 'NONE', *, *, #22184, .T. ) ;
#1866=AXIS2_PLACEMENT_3D ( 'NONE', #21754, #7827, #7933 ) ;
#1874=CARTESIAN_POINT ( 'NONE',  ( -22.62276587825132168, 4.159918992556371542, 9.099611153187048274 ) ) ;
#1879=CARTESIAN_POINT ( 'NONE',  ( -25.00000000000000355, 0.3288899015253046731, 9.999999999999998224 ) ) ;
#1896=EDGE_CURVE ( 'NONE', #5175, #645, #5150, .T. ) ;
#1909=AXIS2_PLACEMENT_3D ( 'NONE', #13871, #3496, #20254 ) ;
#1914=ORIENTED_EDGE ( 'NONE', *, *, #4731, .F. ) ;
#1930=VERTEX_POINT ( 'NONE', #13381 ) ;
#1944=TOROIDAL_SURFACE ( 'NONE', #16681, 22.63401512838748175, 3.000000000000002665 ) ;
#1992=CARTESIAN_POINT ( 'NONE',  ( -23.02469226963562576, 9.740049813577488891, -2.289467137130462238 ) ) ;
#2006=ORIENTED_EDGE ( 'NONE', *, *, #15250, .F. ) ;
#2013=( GEOMETRIC_REPRESENTATION_CONTEXT ( 3 ) GLOBAL_UNCERTAINTY_ASSIGNED_CONTEXT ( ( #9656 ) ) GLOBAL_UNIT_ASSIGNED_CONTEXT ( ( #18358, #8125, #14991 ) ) REPRESENTATION_CONTEXT ( 'NONE', 'WORKASPACE' ) );
#2019=FACE_OUTER_BOUND ( 'NONE', #6808, .T. ) ;
#2025=ORIENTED_EDGE ( 'NONE', *, *, #1211, .T. ) ;
#2034=CARTESIAN_POINT ( 'NONE',  ( 1.387778780781446180E-13, -19.80000000000006111, -78.50000000000000000 ) ) ;
#2038=EDGE_CURVE ( 'NONE', #11804, #19581, #442, .T. ) ;
#2064=VERTEX_POINT ( 'NONE', #20223 ) ;
#2069=DIRECTION ( 'NONE',  ( -0.000000000000000000, 0.000000000000000000, -1.000000000000000000 ) ) ;
#2097=DIRECTION ( 'NONE',  ( -6.982962677686272233E-15, 1.000000000000000000, 0.000000000000000000 ) ) ;
#2098=DIRECTION ( 'NONE',  ( 0.000000000000000000, 0.000000000000000000, -1.000000000000000000 ) ) ;
#2101=SURFACE_SIDE_STYLE ('',( #15737 ) ) ;
#2102=CARTESIAN_POINT ( 'NONE',  ( -24.65444200344273895, 4.153573317486630501, 9.102483954860396409 ) ) ;
#2105=VECTOR ( 'NONE', #3987, 1000.000000000000000 ) ;
#2106=DIRECTION ( 'NONE',  ( 0.000000000000000000, 0.000000000000000000, -1.000000000000000000 ) ) ;
#2109=EDGE_CURVE ( 'NONE', #8590, #10116, #1512, .T. ) ;
#2115=DIRECTION ( 'NONE',  ( -1.000000000000000000, 0.000000000000000000, 0.000000000000000000 ) ) ;
#2116=EDGE_LOOP ( 'NONE', ( #95, #7084, #17209, #11400 ) ) ;
#2121=ADVANCED_FACE ( 'NONE', ( #13615 ), #20452, .T. ) ;
#2156=DIRECTION ( 'NONE',  ( -0.000000000000000000, -1.000000000000000000, -0.000000000000000000 ) ) ;
#2190=DIRECTION ( 'NONE',  ( 0.000000000000000000, -1.000000000000000000, 0.000000000000000000 ) ) ;
#2191=ORIENTED_EDGE ( 'NONE', *, *, #18360, .T. ) ;
#2195=DIRECTION ( 'NONE',  ( -1.000000000000000000, 0.000000000000000000, 0.000000000000000000 ) ) ;
#2208=CARTESIAN_POINT ( 'NONE',  ( -25.00000000000000000, -1.002884296170500229E-19, 10.00000000000000000 ) ) ;
#2211=CARTESIAN_POINT ( 'NONE',  ( 1.232595164407830946E-29, -17.50000000000007105, -30.00000000000000000 ) ) ;
#2228=CIRCLE ( 'NONE', #17321, 3.000000000000002665 ) ;
#2245=ORIENTED_EDGE ( 'NONE', *, *, #11193, .T. ) ;
#2253=LINE ( 'NONE', #19025, #11202 ) ;
#2316=DIRECTION ( 'NONE',  ( -1.000000000000000000, 0.000000000000000000, 0.000000000000000000 ) ) ;
#2319=CARTESIAN_POINT ( 'NONE',  ( 0.000000000000000000, 0.000000000000000000, -24.99999999999999645 ) ) ;
#2324=CARTESIAN_POINT ( 'NONE',  ( 0.000000000000000000, 0.000000000000000000, -75.00000000000000000 ) ) ;
#2327=ORIENTED_EDGE ( 'NONE', *, *, #9143, .F. ) ;
#2334=VERTEX_POINT ( 'NONE', #8774 ) ;
#2349=DIRECTION ( 'NONE',  ( 0.000000000000000000, 0.000000000000000000, -1.000000000000000000 ) ) ;
#2378=DIRECTION ( 'NONE',  ( -0.000000000000000000, 0.000000000000000000, -1.000000000000000000 ) ) ;
#2389=EDGE_CURVE ( 'NONE', #18055, #3468, #17936, .T. ) ;
#2392=ORIENTED_EDGE ( 'NONE', *, *, #13238, .F. ) ;
#2403=FACE_OUTER_BOUND ( 'NONE', #7697, .T. ) ;
#2413=DIRECTION ( 'NONE',  ( 0.000000000000000000, 1.000000000000000000, -0.000000000000000000 ) ) ;
#2422=ORIENTED_EDGE ( 'NONE', *, *, #6882, .F. ) ;
#2433=CARTESIAN_POINT ( 'NONE',  ( 0.000000000000000000, 0.000000000000000000, -60.00000000000000000 ) ) ;
#2440=ORIENTED_EDGE ( 'NONE', *, *, #14341, .F. ) ;
#2456=DIRECTION ( 'NONE',  ( 0.000000000000000000, 0.000000000000000000, -1.000000000000000000 ) ) ;
#2457=CARTESIAN_POINT ( 'NONE',  ( 0.000000000000000000, 23.00000000000006040, 75.00000000000000000 ) ) ;
#2466=EDGE_CURVE ( 'NONE', #14946, #18185, #13256, .T. ) ;
#2471=AXIS2_PLACEMENT_3D ( 'NONE', #3911, #10565, #10684 ) ;
#2478=DIRECTION ( 'NONE',  ( 0.000000000000000000, 0.000000000000000000, -1.000000000000000000 ) ) ;
#2486=CARTESIAN_POINT ( 'NONE',  ( -23.00000000000008882, 0.000000000000000000, 75.00000000000000000 ) ) ;
#2504=CARTESIAN_POINT ( 'NONE',  ( 0.000000000000000000, 22.63401512838754570, -77.51594804401857175 ) ) ;
#2515=VERTEX_POINT ( 'NONE', #542 ) ;
#2519=EDGE_CURVE ( 'NONE', #17072, #12912, #15637, .T. ) ;
#2597=( NAMED_UNIT ( * ) SI_UNIT ( $, .STERADIAN. ) SOLID_ANGLE_UNIT ( ) );
#2613=ORIENTED_EDGE ( 'NONE', *, *, #4471, .T. ) ;
#2625=AXIS2_PLACEMENT_3D ( 'NONE', #18150, #9815, #11392 ) ;
#2631=DIRECTION ( 'NONE',  ( -1.000000000000000000, 0.000000000000000000, 0.000000000000000000 ) ) ;
#2638=PRODUCT_CONTEXT ( 'NONE', #9447, 'mechanical' ) ;
#2642=ORIENTED_EDGE ( 'NONE', *, *, #14893, .T. ) ;
#2646=CARTESIAN_POINT ( 'NONE',  ( -22.17655517979967783, 6.104744444143960891, -7.926958773079715748 ) ) ;
#2660=FACE_OUTER_BOUND ( 'NONE', #3609, .T. ) ;
#2677=CARTESIAN_POINT ( 'NONE',  ( -22.85322867788590528, -2.613756811604178942, -9.658044004399586768 ) ) ;
#2678=CIRCLE ( 'NONE', #15285, 3.000000000000002665 ) ;
#2679=DIRECTION ( 'NONE',  ( -1.000000000000000000, 0.000000000000000000, 0.000000000000000000 ) ) ;
#2707=DIRECTION ( 'NONE',  ( 1.000000000000000000, 0.000000000000000000, 0.000000000000000000 ) ) ;
#2713=COLOUR_RGB ( '', 0.66274510, 0.83137255, 0.94901961) ;
#2740=CARTESIAN_POINT ( 'NONE',  ( 0.000000000000000000, 0.000000000000000000, -69.99999999999998579 ) ) ;
#2748=ORIENTED_EDGE ( 'NONE', *, *, #4317, .T. ) ;
#2752=CARTESIAN_POINT ( 'NONE',  ( -22.85884317627467865, 2.625043582381284324, -9.671636207060540613 ) ) ;
#2766=ORIENTED_EDGE ( 'NONE', *, *, #18879, .F. ) ;
#2768=CARTESIAN_POINT ( 'NONE',  ( 0.000000000000000000, 0.000000000000000000, -77.51594804401857175 ) ) ;
#2769=EDGE_LOOP ( 'NONE', ( #21509, #11219, #17546, #11721 ) ) ;
#2783=CARTESIAN_POINT ( 'NONE',  ( 0.000000000000000000, 19.80000000000006111, -78.50000000000000000 ) ) ;
#2784=DIRECTION ( 'NONE',  ( -1.000000000000000000, 0.000000000000000000, 0.000000000000000000 ) ) ;
#2798=EDGE_CURVE ( 'NONE', #12893, #5175, #6147, .T. ) ;
#2816=FILL_AREA_STYLE_COLOUR ( '', #2713 ) ;
#2856=CARTESIAN_POINT ( 'NONE',  ( -22.94181006055967131, -9.934448251827856069, -1.319932347539896966 ) ) ;
#2890=CARTESIAN_POINT ( 'NONE',  ( 2.465190328815661892E-29, 25.00000000000012790, 75.00000000000000000 ) ) ;
#2899=DIRECTION ( 'NONE',  ( 0.000000000000000000, 0.000000000000000000, -1.000000000000000000 ) ) ;
#2906=EDGE_CURVE ( 'NONE', #1838, #4211, #5700, .T. ) ;
#2936=TOROIDAL_SURFACE ( 'NONE', #20926, 24.63401512838747820, 3.000000000000000888 ) ;
#2939=EDGE_CURVE ( 'NONE', #2334, #20174, #21148, .T. ) ;
#2956=CIRCLE ( 'NONE', #14142, 23.00000000000008882 ) ;
#2968=CARTESIAN_POINT ( 'NONE',  ( -22.91279148301329016, -10.00019932322032723, 0.3240289003878054630 ) ) ;
#2975=AXIS2_PLACEMENT_3D ( 'NONE', #19668, #5948, #6056 ) ;
#2987=ORIENTED_EDGE ( 'NONE', *, *, #8940, .T. ) ;
#2994=CIRCLE ( 'NONE', #17751, 21.80000000000008598 ) ;
#3001=CARTESIAN_POINT ( 'NONE',  ( 1.526556658859591000E-13, -22.63401512838754570, -77.51594804401857175 ) ) ;
#3013=AXIS2_PLACEMENT_3D ( 'NONE', #3894, #14047, #13709 ) ;
#3034=ADVANCED_FACE ( 'NONE', ( #2660 ), #12697, .F. ) ;
#3068=DIRECTION ( 'NONE',  ( -1.000000000000000000, 0.000000000000000000, 0.000000000000000000 ) ) ;
#3080=EDGE_CURVE ( 'NONE', #21835, #12695, #14616, .T. ) ;
#3086=LINE ( 'NONE', #14810, #9503 ) ;
#3093=PLANE ( 'NONE',  #14487 ) ;
#3109=UNCERTAINTY_MEASURE_WITH_UNIT (LENGTH_MEASURE( 1.000000000000000082E-05 ), #15845, 'distance_accuracy_value', 'NONE');
#3117=CARTESIAN_POINT ( 'NONE',  ( -24.30989004983127799, 5.839958665417457340, -8.124004078861357669 ) ) ;
#3144=DIRECTION ( 'NONE',  ( 1.083936797661038068E-15, 1.000000000000000000, 0.000000000000000000 ) ) ;
#3166=ORIENTED_EDGE ( 'NONE', *, *, #20103, .F. ) ;
#3182=FACE_OUTER_BOUND ( 'NONE', #13047, .T. ) ;
#3200=ADVANCED_FACE ( 'NONE', ( #7633 ), #18989, .F. ) ;
#3210=CARTESIAN_POINT ( 'NONE',  ( 0.000000000000000000, 19.80000000000006111, 78.50000000000000000 ) ) ;
#3216=DIRECTION ( 'NONE',  ( -1.000000000000000000, 0.000000000000000000, 0.000000000000000000 ) ) ;
#3227=CARTESIAN_POINT ( 'NONE',  ( -22.77702959565148788, -3.252406101723253062, 9.478689975477541552 ) ) ;
#3232=ORIENTED_EDGE ( 'NONE', *, *, #6382, .F. ) ;
#3236=VERTEX_POINT ( 'NONE', #21228 ) ;
#3268=DIRECTION ( 'NONE',  ( 0.000000000000000000, 0.000000000000000000, -1.000000000000000000 ) ) ;
#3297=AXIS2_PLACEMENT_3D ( 'NONE', #20564, #22039, #15310 ) ;
#3299=ORIENTED_EDGE ( 'NONE', *, *, #14893, .F. ) ;
#3304=FACE_OUTER_BOUND ( 'NONE', #10785, .T. ) ;
#3330=TOROIDAL_SURFACE ( 'NONE', #6934, 24.63401512838747820, 3.000000000000000888 ) ;
#3333=CIRCLE ( 'NONE', #20207, 23.00000000000008882 ) ;
#3350=DIRECTION ( 'NONE',  ( 0.000000000000000000, 0.000000000000000000, -1.000000000000000000 ) ) ;
#3376=ORIENTED_EDGE ( 'NONE', *, *, #11036, .T. ) ;
#3378=ORIENTED_EDGE ( 'NONE', *, *, #14496, .F. ) ;
#3383=CARTESIAN_POINT ( 'NONE',  ( 0.000000000000000000, -23.00000000000006040, 75.00000000000000000 ) ) ;
#3399=CARTESIAN_POINT ( 'NONE',  ( 0.000000000000000000, 23.00000000000006040, -55.00000000000000711 ) ) ;
#3403=VECTOR ( 'NONE', #6983, 1000.000000000000000 ) ;
#3407=B_SPLINE_CURVE_WITH_KNOTS ( 'NONE', 3,
 ( #11239, #12824, #19667, #16422, #2677, #7649, #16525, #19885, #9338, #18223, #1104, #14844, #21687, #16198, #6278, #4254, #6500, #3455, #4924, #1668, #12021, #10222, #18441, #8543, #1555, #13488, #6388, #5139, #10334, #21911, #22252, #11684, #6845, #8203, #14961, #22027, #6736, #11800, #1219, #21801, #8094, #1331, #11906, #3227, #20551, #6618, #16975, #13260 ),
 .UNSPECIFIED., .F., .F.,
 ( 4, 2, 2, 2, 2, 2, 2, 2, 2, 2, 2, 2, 2, 2, 2, 2, 2, 2, 2, 2, 2, 2, 2, 4 ),
 ( 1.201007004285936770E-19, 0.001979062126186861923, 0.002968593189280293101, 0.003958124252373724714, 0.005937186378560591407, 0.006926717441654025621, 0.007916248504747461570, 0.008905779567840894917, 0.009895310630934329998, 0.01187437275712120190, 0.01286390382021463698, 0.01385343488330807553, 0.01583249700949494396, 0.01682202807258837904, 0.01781155913568181065, 0.01880109019877524573, 0.01979062126186868081, 0.02176968338805555098, 0.02374874551424242461, 0.02572780764042929824, 0.02671733870352273679, 0.02770686976661617534, 0.02968593189280304898, 0.03166499401898992955 ),
 .UNSPECIFIED. ) ;
#3415=AXIS2_PLACEMENT_3D ( 'NONE', #4146, #4584, #9560 ) ;
#3450=CARTESIAN_POINT ( 'NONE',  ( -22.94283062359114922, 1.652932088558951573, 9.867976570195974517 ) ) ;
#3451=CARTESIAN_POINT ( 'NONE',  ( 0.000000000000000000, 0.000000000000000000, 60.00000000000001421 ) ) ;
#3453=AXIS2_PLACEMENT_3D ( 'NONE', #585, #10608, #7460 ) ;
#3455=CARTESIAN_POINT ( 'NONE',  ( -21.30687190786788676, -8.669990142398665611, -5.025571895822516844 ) ) ;
#3460=ORIENTED_EDGE ( 'NONE', *, *, #8010, .F. ) ;
#3468=VERTEX_POINT ( 'NONE', #8412 ) ;
#3481=CARTESIAN_POINT ( 'NONE',  ( 2.985191413800211088E-29, 21.63401512838760610, -77.51594804401857175 ) ) ;
#3496=DIRECTION ( 'NONE',  ( 0.000000000000000000, 0.000000000000000000, -1.000000000000000000 ) ) ;
#3525=ORIENTED_EDGE ( 'NONE', *, *, #13692, .T. ) ;
#3548=CARTESIAN_POINT ( 'NONE',  ( -25.00000000000000000, 0.000000000000000000, 75.00000000000000000 ) ) ;
#3552=CYLINDRICAL_SURFACE ( 'NONE', #11579, 23.00000000000008882 ) ;
#3560=DIRECTION ( 'NONE',  ( -0.000000000000000000, 0.000000000000000000, -1.000000000000000000 ) ) ;
#3561=CARTESIAN_POINT ( 'NONE',  ( -20.95737978171097993, 9.479626318133300700, 3.249830451118298047 ) ) ;
#3566=CARTESIAN_POINT ( 'NONE',  ( -24.99351254083359208, 0.6581337445957534671, 9.983815384650208458 ) ) ;
#3578=ORIENTED_EDGE ( 'NONE', *, *, #16995, .T. ) ;
#3595=ORIENTED_EDGE ( 'NONE', *, *, #16262, .F. ) ;
#3598=EDGE_CURVE ( 'NONE', #758, #12912, #16124, .T. ) ;
#3609=EDGE_LOOP ( 'NONE', ( #11113, #11248, #19713, #2392 ) ) ;
#3615=FACE_OUTER_BOUND ( 'NONE', #253, .T. ) ;
#3650=FACE_OUTER_BOUND ( 'NONE', #20250, .T. ) ;
#3664=CARTESIAN_POINT ( 'NONE',  ( -22.44443514569313081, 5.033247747886526291, 8.647138457592827621 ) ) ;
#3667=DIRECTION ( 'NONE',  ( 0.000000000000000000, -1.000000000000000000, 0.000000000000000000 ) ) ;
#3672=LINE ( 'NONE', #320, #8873 ) ;
#3676=ORIENTED_EDGE ( 'NONE', *, *, #8689, .T. ) ;
#3682=VERTEX_POINT ( 'NONE', #4904 ) ;
#3691=DIRECTION ( 'NONE',  ( 0.000000000000000000, 0.000000000000000000, -1.000000000000000000 ) ) ;
#3704=ORIENTED_EDGE ( 'NONE', *, *, #11353, .F. ) ;
#3712=DIRECTION ( 'NONE',  ( -0.000000000000000000, 0.000000000000000000, -1.000000000000000000 ) ) ;
#3713=FACE_OUTER_BOUND ( 'NONE', #10038, .T. ) ;
#3715=VECTOR ( 'NONE', #6158, 1000.000000000000000 ) ;
#3726=DIRECTION ( 'NONE',  ( -1.000000000000000000, 0.000000000000000000, 0.000000000000000000 ) ) ;
#3735=AXIS2_PLACEMENT_3D ( 'NONE', #3451, #6496, #8200 ) ;
#3743=ORIENTED_EDGE ( 'NONE', *, *, #15073, .F. ) ;
#3746=VERTEX_POINT ( 'NONE', #18649 ) ;
#3760=VERTEX_POINT ( 'NONE', #3210 ) ;
#3764=EDGE_CURVE ( 'NONE', #18119, #1644, #21848, .T. ) ;
#3766=LINE ( 'NONE', #5233, #14334 ) ;
#3783=CARTESIAN_POINT ( 'NONE',  ( 0.000000000000000000, -23.00000000000006040, -30.00000000000000000 ) ) ;
#3784=CARTESIAN_POINT ( 'NONE',  ( 0.000000000000000000, 0.000000000000000000, -77.51594804401857175 ) ) ;
#3787=FILL_AREA_STYLE_COLOUR ( '', #4518 ) ;
#3791=CARTESIAN_POINT ( 'NONE',  ( -21.80000000000008242, 0.000000000000000000, 78.50000000000000000 ) ) ;
#3794=ORIENTED_EDGE ( 'NONE', *, *, #11758, .T. ) ;
#3813=FACE_OUTER_BOUND ( 'NONE', #2116, .T. ) ;
#3841=DIRECTION ( 'NONE',  ( 0.000000000000000000, 0.000000000000000000, -1.000000000000000000 ) ) ;
#3842=EDGE_CURVE ( 'NONE', #10586, #16331, #3766, .T. ) ;
#3862=VERTEX_POINT ( 'NONE', #10651 ) ;
#3869=DIRECTION ( 'NONE',  ( 0.000000000000000000, 0.000000000000000000, -1.000000000000000000 ) ) ;
#3892=CARTESIAN_POINT ( 'NONE',  ( -24.86551311171973566, -2.609124161958199739, -9.659280632943737288 ) ) ;
#3894=CARTESIAN_POINT ( 'NONE',  ( 0.000000000000000000, 0.000000000000000000, -78.50000000000000000 ) ) ;
#3902=CARTESIAN_POINT ( 'NONE',  ( 0.000000000000000000, 23.00000000000006040, 69.99999999999998579 ) ) ;
#3909=ORIENTED_EDGE ( 'NONE', *, *, #2466, .F. ) ;
#3911=CARTESIAN_POINT ( 'NONE',  ( 0.000000000000000000, 0.000000000000000000, -60.00000000000000000 ) ) ;
#3933=ORIENTED_EDGE ( 'NONE', *, *, #15250, .T. ) ;
#3939=CARTESIAN_POINT ( 'NONE',  ( 1.387778780781446180E-13, -19.80000000000006111, -78.50000000000000000 ) ) ;
#3950=CARTESIAN_POINT ( 'NONE',  ( 0.000000000000000000, 0.000000000000000000, -77.51594804401857175 ) ) ;
#3959=DIRECTION ( 'NONE',  ( -0.000000000000000000, 0.000000000000000000, -1.000000000000000000 ) ) ;
#3972=DIRECTION ( 'NONE',  ( 4.408728476930457445E-15, -1.000000000000000000, 0.000000000000000000 ) ) ;
#3987=DIRECTION ( 'NONE',  ( -0.000000000000000000, 0.000000000000000000, -1.000000000000000000 ) ) ;
#3996=ORIENTED_EDGE ( 'NONE', *, *, #6636, .F. ) ;
#4024=CIRCLE ( 'NONE', #16608, 19.63401512838747820 ) ;
#4039=ORIENTED_EDGE ( 'NONE', *, *, #13717, .T. ) ;
#4047=EDGE_CURVE ( 'NONE', #15083, #21835, #16844, .T. ) ;
#4050=EDGE_CURVE ( 'NONE', #2515, #1930, #10862, .T. ) ;
#4102=DIRECTION ( 'NONE',  ( -1.000000000000000000, 0.000000000000000000, 0.000000000000000000 ) ) ;
#4107=SHAPE_DEFINITION_REPRESENTATION ( #79, #14642 ) ;
#4118=FILL_AREA_STYLE ('',( #3787 ) ) ;
#4122=CARTESIAN_POINT ( 'NONE',  ( 1.665334536937735316E-13, -24.63401512838760610, 77.51594804401857175 ) ) ;
#4131=CARTESIAN_POINT ( 'NONE',  ( 0.000000000000000000, 0.000000000000000000, -24.99999999999999645 ) ) ;
#4146=CARTESIAN_POINT ( 'NONE',  ( 0.000000000000000000, 0.000000000000000000, 78.50000000000000000 ) ) ;
#4147=DIRECTION ( 'NONE',  ( 0.000000000000000000, 0.000000000000000000, -1.000000000000000000 ) ) ;
#4178=DIRECTION ( 'NONE',  ( 0.000000000000000000, 0.000000000000000000, 1.000000000000000000 ) ) ;
#4200=DIRECTION ( 'NONE',  ( 0.000000000000000000, 0.000000000000000000, -1.000000000000000000 ) ) ;
#4211=VERTEX_POINT ( 'NONE', #3548 ) ;
#4221=CARTESIAN_POINT ( 'NONE',  ( 0.000000000000000000, 0.000000000000000000, -78.50000000000000000 ) ) ;
#4222=CARTESIAN_POINT ( 'NONE',  ( -22.99261559126758314, 0.6704778918838653068, -9.983049392048402026 ) ) ;
#4247=EDGE_CURVE ( 'NONE', #20174, #17900, #5341, .T. ) ;
#4254=CARTESIAN_POINT ( 'NONE',  ( -21.59054411123144135, -7.930690890291152151, -6.099882278136012026 ) ) ;
#4262=ORIENTED_EDGE ( 'NONE', *, *, #3598, .F. ) ;
#4275=DIRECTION ( 'NONE',  ( -1.000000000000000000, 0.000000000000000000, 0.000000000000000000 ) ) ;
#4281=ADVANCED_FACE ( 'NONE', ( #3650 ), #17199, .F. ) ;
#4312=CARTESIAN_POINT ( 'NONE',  ( 0.000000000000000000, 0.000000000000000000, -60.00000000000001421 ) ) ;
#4317=EDGE_CURVE ( 'NONE', #18628, #1930, #10534, .T. ) ;
#4324=CARTESIAN_POINT ( 'NONE',  ( -22.91992063051224449, -9.983913345421759900, 0.6574913861358061551 ) ) ;
#4349=CARTESIAN_POINT ( 'NONE',  ( -23.13858343966594688, 9.466612565523535139, -3.238977037839615214 ) ) ;
#4386=CIRCLE ( 'NONE', #13033, 23.00000000000008882 ) ;
#4418=CIRCLE ( 'NONE', #831, 3.000000000000002665 ) ;
#4436=CARTESIAN_POINT ( 'NONE',  ( -24.74809011923674262, -3.553243708740094320, -9.353164043501660530 ) ) ;
#4455=DIRECTION ( 'NONE',  ( -1.000000000000000000, 0.000000000000000000, 0.000000000000000000 ) ) ;
#4456=ORIENTED_EDGE ( 'NONE', *, *, #17479, .T. ) ;
#4467=CARTESIAN_POINT ( 'NONE',  ( -24.60613290926164609, 4.462958844126968749, -8.973150446544476466 ) ) ;
#4471=EDGE_CURVE ( 'NONE', #7333, #3862, #7868, .T. ) ;
#4492=VECTOR ( 'NONE', #6161, 1000.000000000000000 ) ;
#4494=CIRCLE ( 'NONE', #13494, 3.000000000000002665 ) ;
#4510=AXIS2_PLACEMENT_3D ( 'NONE', #16453, #4178, #914 ) ;
#4518=COLOUR_RGB ( '', 0.66274510, 0.83137255, 0.94901961) ;
#4519=ORIENTED_EDGE ( 'NONE', *, *, #14391, .T. ) ;
#4530=DIRECTION ( 'NONE',  ( 0.000000000000000000, 0.000000000000000000, -1.000000000000000000 ) ) ;
#4552=CARTESIAN_POINT ( 'NONE',  ( 1.232595164407830946E-29, -17.50000000000007105, -60.00000000000000000 ) ) ;
#4564=VERTEX_POINT ( 'NONE', #16051 ) ;
#4569=CARTESIAN_POINT ( 'NONE',  ( 0.000000000000000000, 0.000000000000000000, 75.00000000000000000 ) ) ;
#4584=DIRECTION ( 'NONE',  ( -0.000000000000000000, 0.000000000000000000, -1.000000000000000000 ) ) ;
#4608=FACE_OUTER_BOUND ( 'NONE', #9012, .T. ) ;
#4616=DIRECTION ( 'NONE',  ( -0.000000000000000000, 0.000000000000000000, -1.000000000000000000 ) ) ;
#4632=ORIENTED_EDGE ( 'NONE', *, *, #7205, .F. ) ;
#4652=EDGE_CURVE ( 'NONE', #10566, #20364, #2228, .T. ) ;
#4660=CARTESIAN_POINT ( 'NONE',  ( -23.84329938582383690, -7.531468209848477535, -6.610083113334743743 ) ) ;
#4676=ORIENTED_EDGE ( 'NONE', *, *, #983, .T. ) ;
#4683=CARTESIAN_POINT ( 'NONE',  ( -2.465190328815661892E-29, -25.00000000000012790, 75.00000000000000000 ) ) ;
#4685=EDGE_CURVE ( 'NONE', #324, #12893, #18393, .T. ) ;
#4687=CARTESIAN_POINT ( 'NONE',  ( -23.33796567949162082, 8.964750604579641902, -4.443019783309294368 ) ) ;
#4692=CYLINDRICAL_SURFACE ( 'NONE', #20597, 21.00000000000008171 ) ;
#4722=ADVANCED_FACE ( 'NONE', ( #12882 ), #19732, .F. ) ;
#4730=AXIS2_PLACEMENT_3D ( 'NONE', #16261, #19515, #4102 ) ;
#4731=EDGE_CURVE ( 'NONE', #15638, #10545, #11213, .T. ) ;
#4753=B_SPLINE_CURVE_WITH_KNOTS ( 'NONE', 3,
 ( #10771, #8978, #12237, #17637, #3450, #17299, #15842, #1874, #19088, #3664, #1769, #418, #10330, #10550, #17419, #8643, #17192, #15504, #20663, #5245, #12127, #3561, #18074, #9633, #13004, #7405, #965, #7616, #14484, #14705, #12792, #11102, #21539, #19850, #636, #14275, #21107, #2646, #6024, #12572, #12897, #21213, #7512, #12680, #2752, #14379, #16275, #4222, #11208, #5799 ),
 .UNSPECIFIED., .F., .F.,
 ( 4, 2, 2, 2, 2, 2, 2, 2, 2, 2, 2, 2, 2, 2, 2, 2, 2, 2, 2, 2, 2, 2, 2, 2, 4 ),
 ( 0.03166499401898992955, 0.03265355373879610251, 0.03364211345860227548, 0.03561923289821462141, 0.03660779261802078743, 0.03759635233782696040, 0.03858491205763313336, 0.03957347177743930633, 0.04155059121705165226, 0.04253915093685782522, 0.04352771065666399819, 0.04550483009627633718, 0.04649338981608251015, 0.04748194953588867617, 0.04945906897550102210, 0.05143618841511336803, 0.05341330785472571396, 0.05539042729433805989, 0.05637898701414422592, 0.05736754673395039889, 0.05835610645375657185, 0.05934466617356273788, 0.06132178561317508381, 0.06231034533298125677, 0.06329890505278742974 ),
 .UNSPECIFIED. ) ;
#4759=AXIS2_PLACEMENT_3D ( 'NONE', #10909, #12825, #2679 ) ;
#4768=ORIENTED_EDGE ( 'NONE', *, *, #21373, .T. ) ;
#4771=CARTESIAN_POINT ( 'NONE',  ( -24.24407467525207238, -6.106727297653192110, -7.925496382379915161 ) ) ;
#4772=DIRECTION ( 'NONE',  ( 0.000000000000000000, 1.000000000000000000, -0.000000000000000000 ) ) ;
#4796=AXIS2_PLACEMENT_3D ( 'NONE', #6724, #5020, #1207 ) ;
#4797=VECTOR ( 'NONE', #2097, 1000.000000000000000 ) ;
#4803=CARTESIAN_POINT ( 'NONE',  ( -24.04585643156664077, 6.844992825942523673, -7.297348454157751796 ) ) ;
#4817=EDGE_LOOP ( 'NONE', ( #6352, #1844, #564, #21444 ) ) ;
#4860=ORIENTED_EDGE ( 'NONE', *, *, #5761, .F. ) ;
#4884=ORIENTED_EDGE ( 'NONE', *, *, #7094, .F. ) ;
#4899=ORIENTED_EDGE ( 'NONE', *, *, #11585, .F. ) ;
#4904=CARTESIAN_POINT ( 'NONE',  ( 1.526556658859590496E-13, -21.80000000000006111, 78.50000000000000000 ) ) ;
#4910=CYLINDRICAL_SURFACE ( 'NONE', #5521, 23.00000000000008882 ) ;
#4924=CARTESIAN_POINT ( 'NONE',  ( -21.17788351146302617, -8.976196367870899806, -4.455375687320114686 ) ) ;
#4948=DIRECTION ( 'NONE',  ( 0.000000000000000000, 0.000000000000000000, 1.000000000000000000 ) ) ;
#4997=DIRECTION ( 'NONE',  ( 0.000000000000000000, 0.000000000000000000, 1.000000000000000000 ) ) ;
#5011=ADVANCED_FACE ( 'NONE', ( #7965 ), #14725, .T. ) ;
#5020=DIRECTION ( 'NONE',  ( 0.000000000000000000, 0.000000000000000000, 1.000000000000000000 ) ) ;
#5029=CARTESIAN_POINT ( 'NONE',  ( -1.232595164407830946E-29, 17.50000000000007105, -60.00000000000000000 ) ) ;
#5041=CARTESIAN_POINT ( 'NONE',  ( 1.387778780781446180E-13, -19.80000000000006111, -78.50000000000000000 ) ) ;
#5054=CARTESIAN_POINT ( 'NONE',  ( -17.50000000000000711, 0.000000000000000000, -24.99999999999999645 ) ) ;
#5115=AXIS2_PLACEMENT_3D ( 'NONE', #20354, #18468, #3144 ) ;
#5133=DIRECTION ( 'NONE',  ( 0.000000000000000000, 0.000000000000000000, 1.000000000000000000 ) ) ;
#5135=LINE ( 'NONE', #20547, #872 ) ;
#5139=CARTESIAN_POINT ( 'NONE',  ( -20.75182054862913006, -9.917826596856404109, 1.322042766941443626 ) ) ;
#5142=EDGE_CURVE ( 'NONE', #8407, #11804, #15175, .T. ) ;
#5150=LINE ( 'NONE', #8213, #16618 ) ;
#5151=VECTOR ( 'NONE', #18428, 1000.000000000000000 ) ;
#5152=ORIENTED_EDGE ( 'NONE', *, *, #22017, .T. ) ;
#5153=CIRCLE ( 'NONE', #20226, 21.00000000000008527 ) ;
#5164=LINE ( 'NONE', #8338, #3403 ) ;
#5175=VERTEX_POINT ( 'NONE', #22008 ) ;
#5181=DIRECTION ( 'NONE',  ( 1.000000000000000000, 0.000000000000000000, 0.000000000000000000 ) ) ;
#5185=ADVANCED_FACE ( 'NONE', ( #10321 ), #6944, .F. ) ;
#5188=ORIENTED_EDGE ( 'NONE', *, *, #15930, .T. ) ;
#5203=DIRECTION ( 'NONE',  ( 0.000000000000000000, 0.000000000000000000, -1.000000000000000000 ) ) ;
#5210=AXIS2_PLACEMENT_3D ( 'NONE', #14631, #14520, #21354 ) ;
#5233=CARTESIAN_POINT ( 'NONE',  ( 0.000000000000000000, 21.00000000000006395, 75.00000000000000000 ) ) ;
#5245=CARTESIAN_POINT ( 'NONE',  ( -21.18273580851505145, 8.962137229497693980, 4.448298016007305122 ) ) ;
#5249=DIRECTION ( 'NONE',  ( -1.000000000000000000, 0.000000000000000000, 0.000000000000000000 ) ) ;
#5274=DIRECTION ( 'NONE',  ( 0.000000000000000000, 0.000000000000000000, 1.000000000000000000 ) ) ;
#5283=EDGE_LOOP ( 'NONE', ( #18489, #9456, #17732, #12070, #11506, #9170 ) ) ;
#5291=FACE_OUTER_BOUND ( 'NONE', #17619, .T. ) ;
#5304=DIRECTION ( 'NONE',  ( -1.000000000000000000, 0.000000000000000000, 0.000000000000000000 ) ) ;
#5341=LINE ( 'NONE', #12223, #10018 ) ;
#5342=ORIENTED_EDGE ( 'NONE', *, *, #4652, .T. ) ;
#5353=CARTESIAN_POINT ( 'NONE',  ( 1.665334536937735316E-13, -24.63401512838760610, 77.51594804401857175 ) ) ;
#5381=DIRECTION ( 'NONE',  ( -1.000000000000000000, 0.000000000000000000, 0.000000000000000000 ) ) ;
#5389=EDGE_LOOP ( 'NONE', ( #8142, #17844, #20869, #7146, #830, #18701 ) ) ;
#5395=LINE ( 'NONE', #6568, #5437 ) ;
#5397=CARTESIAN_POINT ( 'NONE',  ( 0.000000000000000000, 0.000000000000000000, -77.51594804401857175 ) ) ;
#5414=CYLINDRICAL_SURFACE ( 'NONE', #10653, 10.00000000000000000 ) ;
#5432=ORIENTED_EDGE ( 'NONE', *, *, #4050, .T. ) ;
#5435=ORIENTED_EDGE ( 'NONE', *, *, #18082, .F. ) ;
#5437=VECTOR ( 'NONE', #10814, 1000.000000000000000 ) ;
#5447=ORIENTED_EDGE ( 'NONE', *, *, #198, .F. ) ;
#5453=DIRECTION ( 'NONE',  ( 0.000000000000000000, 0.000000000000000000, -1.000000000000000000 ) ) ;
#5454=ORIENTED_EDGE ( 'NONE', *, *, #6882, .T. ) ;
#5474=CARTESIAN_POINT ( 'NONE',  ( -23.70658472240227255, 7.946283115275369013, 6.105263035233634561 ) ) ;
#5480=EDGE_LOOP ( 'NONE', ( #3232, #17739, #11618, #12233 ) ) ;
#5484=ORIENTED_EDGE ( 'NONE', *, *, #8689, .F. ) ;
#5492=AXIS2_PLACEMENT_3D ( 'NONE', #20986, #8964, #12337 ) ;
#5521=AXIS2_PLACEMENT_3D ( 'NONE', #11789, #18655, #3216 ) ;
#5532=EDGE_CURVE ( 'NONE', #18185, #20995, #13591, .T. ) ;
#5577=FACE_OUTER_BOUND ( 'NONE', #5389, .T. ) ;
#5579=AXIS2_PLACEMENT_3D ( 'NONE', #8457, #8669, #6525 ) ;
#5585=ORIENTED_EDGE ( 'NONE', *, *, #13649, .F. ) ;
#5588=CARTESIAN_POINT ( 'NONE',  ( -22.63401512838757057, 0.000000000000000000, -77.51594804401857175 ) ) ;
#5610=AXIS2_PLACEMENT_3D ( 'NONE', #16389, #6471, #11211 ) ;
#5645=DIRECTION ( 'NONE',  ( 0.000000000000000000, 0.000000000000000000, -1.000000000000000000 ) ) ;
#5657=ADVANCED_FACE ( 'NONE', ( #5577 ), #3552, .F. ) ;
#5680=CYLINDRICAL_SURFACE ( 'NONE', #5492, 17.50000000000007816 ) ;
#5700=CIRCLE ( 'NONE', #10037, 25.00000000000010303 ) ;
#5704=ORIENTED_EDGE ( 'NONE', *, *, #5532, .F. ) ;
#5711=ORIENTED_EDGE ( 'NONE', *, *, #2519, .T. ) ;
#5748=DIRECTION ( 'NONE',  ( -0.000000000000000000, 0.000000000000000000, -1.000000000000000000 ) ) ;
#5761=EDGE_CURVE ( 'NONE', #17900, #8590, #14036, .T. ) ;
#5768=EDGE_LOOP ( 'NONE', ( #8989, #3794, #2006, #11869 ) ) ;
#5769=CARTESIAN_POINT ( 'NONE',  ( 0.000000000000000000, 0.000000000000000000, -78.50000000000000000 ) ) ;
#5775=DIRECTION ( 'NONE',  ( -0.000000000000000000, -0.000000000000000000, -1.000000000000000000 ) ) ;
#5780=ORIENTED_EDGE ( 'NONE', *, *, #6636, .T. ) ;
#5799=CARTESIAN_POINT ( 'NONE',  ( -23.00000000000006750, -1.237926774615798086E-16, -10.00000000000000000 ) ) ;
#5816=ORIENTED_EDGE ( 'NONE', *, *, #17196, .T. ) ;
#5834=CARTESIAN_POINT ( 'NONE',  ( -23.00000000000008882, 0.000000000000000000, 75.00000000000000000 ) ) ;
#5853=AXIS2_PLACEMENT_3D ( 'NONE', #13532, #22072, #17021 ) ;
#5868=CIRCLE ( 'NONE', #131, 3.000000000000002665 ) ;
#5869=AXIS2_PLACEMENT_3D ( 'NONE', #12923, #992, #7866 ) ;
#5915=CARTESIAN_POINT ( 'NONE',  ( 0.000000000000000000, 0.000000000000000000, -75.00000000000000000 ) ) ;
#5930=CARTESIAN_POINT ( 'NONE',  ( 0.000000000000000000, 23.00000000000006040, -69.99999999999998579 ) ) ;
#5931=CIRCLE ( 'NONE', #3415, 21.80000000000008598 ) ;
#5937=DIRECTION ( 'NONE',  ( -1.000000000000000000, 0.000000000000000000, 0.000000000000000000 ) ) ;
#5948=DIRECTION ( 'NONE',  ( 0.000000000000000000, 0.000000000000000000, 1.000000000000000000 ) ) ;
#5964=AXIS2_PLACEMENT_3D ( 'NONE', #10827, #2378, #7354 ) ;
#6005=EDGE_LOOP ( 'NONE', ( #6256, #20651, #15858, #3909 ) ) ;
#6014=DIRECTION ( 'NONE',  ( 0.000000000000000000, 0.000000000000000000, 1.000000000000000000 ) ) ;
#6023=FACE_OUTER_BOUND ( 'NONE', #16405, .T. ) ;
#6024=CARTESIAN_POINT ( 'NONE',  ( -22.24636130842955595, 5.845994931192185717, -8.119638057951140908 ) ) ;
#6056=DIRECTION ( 'NONE',  ( 1.000000000000000000, 0.000000000000000000, 0.000000000000000000 ) ) ;
#6065=DIRECTION ( 'NONE',  ( -1.000000000000000000, 0.000000000000000000, 0.000000000000000000 ) ) ;
#6077=CARTESIAN_POINT ( 'NONE',  ( 0.000000000000000000, 0.000000000000000000, -60.00000000000000000 ) ) ;
#6089=EDGE_CURVE ( 'NONE', #11804, #758, #17648, .T. ) ;
#6117=CARTESIAN_POINT ( 'NONE',  ( 1.232595164407830946E-29, -17.50000000000007105, -24.99999999999999645 ) ) ;
#6126=VERTEX_POINT ( 'NONE', #9731 ) ;
#6139=DIRECTION ( 'NONE',  ( 1.000000000000000000, 0.000000000000000000, 0.000000000000000000 ) ) ;
#6142=ORIENTED_EDGE ( 'NONE', *, *, #6089, .F. ) ;
#6147=LINE ( 'NONE', #5930, #15424 ) ;
#6156=CARTESIAN_POINT ( 'NONE',  ( -24.96693800283771836, 1.326846381236610473, -9.917101879163732647 ) ) ;
#6158=DIRECTION ( 'NONE',  ( -0.000000000000000000, 0.000000000000000000, -1.000000000000000000 ) ) ;
#6161=DIRECTION ( 'NONE',  ( -0.000000000000000000, 0.000000000000000000, -1.000000000000000000 ) ) ;
#6163=DIRECTION ( 'NONE',  ( -0.000000000000000000, 0.000000000000000000, -1.000000000000000000 ) ) ;
#6172=DIRECTION ( 'NONE',  ( 0.000000000000000000, 0.000000000000000000, 1.000000000000000000 ) ) ;
#6206=VECTOR ( 'NONE', #1708, 1000.000000000000000 ) ;
#6220=DIRECTION ( 'NONE',  ( 0.000000000000000000, 0.000000000000000000, -1.000000000000000000 ) ) ;
#6232=DIRECTION ( 'NONE',  ( -1.000000000000000000, 0.000000000000000000, 0.000000000000000000 ) ) ;
#6242=EDGE_LOOP ( 'NONE', ( #6509, #8810, #22156, #16186 ) ) ;
#6256=ORIENTED_EDGE ( 'NONE', *, *, #11758, .F. ) ;
#6263=ORIENTED_EDGE ( 'NONE', *, *, #5142, .T. ) ;
#6273=CARTESIAN_POINT ( 'NONE',  ( -25.00000000000000000, 0.000000000000000000, -75.00000000000000000 ) ) ;
#6278=CARTESIAN_POINT ( 'NONE',  ( -21.73688349724618263, -7.520329038248549480, -6.599172142090282911 ) ) ;
#6352=ORIENTED_EDGE ( 'NONE', *, *, #10914, .F. ) ;
#6372=ORIENTED_EDGE ( 'NONE', *, *, #10264, .F. ) ;
#6382=EDGE_CURVE ( 'NONE', #3862, #10678, #4024, .T. ) ;
#6384=DIRECTION ( 'NONE',  ( 0.000000000000000000, 0.000000000000000000, -1.000000000000000000 ) ) ;
#6388=CARTESIAN_POINT ( 'NONE',  ( -20.72013996799678637, -9.983843958838708232, 0.6587422018470180385 ) ) ;
#6399=DIRECTION ( 'NONE',  ( -1.000000000000000000, 0.000000000000000000, 0.000000000000000000 ) ) ;
#6453=CARTESIAN_POINT ( 'NONE',  ( 0.000000000000000000, 0.000000000000000000, 77.51594804401857175 ) ) ;
#6466=CARTESIAN_POINT ( 'NONE',  ( -25.00000000000000355, -0.3291058866677926686, 10.00000000000000178 ) ) ;
#6471=DIRECTION ( 'NONE',  ( -0.000000000000000000, 0.000000000000000000, -1.000000000000000000 ) ) ;
#6474=FACE_OUTER_BOUND ( 'NONE', #21415, .T. ) ;
#6488=LINE ( 'NONE', #4683, #223 ) ;
#6494=CARTESIAN_POINT ( 'NONE',  ( 2.465190328815661892E-29, 25.00000000000012790, 75.00000000000000000 ) ) ;
#6496=DIRECTION ( 'NONE',  ( 0.000000000000000000, 0.000000000000000000, 1.000000000000000000 ) ) ;
#6499=EDGE_CURVE ( 'NONE', #21649, #17512, #13883, .T. ) ;
#6500=CARTESIAN_POINT ( 'NONE',  ( -21.51775537703705155, -8.125520501844063048, -5.837995551681642858 ) ) ;
#6509=ORIENTED_EDGE ( 'NONE', *, *, #11837, .F. ) ;
#6515=EDGE_CURVE ( 'NONE', #9399, #11804, #9576, .T. ) ;
#6525=DIRECTION ( 'NONE',  ( -1.000000000000000000, 0.000000000000000000, 0.000000000000000000 ) ) ;
#6526=LINE ( 'NONE', #10027, #13387 ) ;
#6538=EDGE_CURVE ( 'NONE', #1838, #17384, #6488, .T. ) ;
#6558=DIRECTION ( 'NONE',  ( -0.000000000000000000, 0.000000000000000000, -1.000000000000000000 ) ) ;
#6568=CARTESIAN_POINT ( 'NONE',  ( -17.50000000000007816, 0.000000000000000000, -24.99999999999999645 ) ) ;
#6586=AXIS2_PLACEMENT_3D ( 'NONE', #12281, #19766, #5937 ) ;
#6594=ORIENTED_EDGE ( 'NONE', *, *, #8422, .T. ) ;
#6596=EDGE_CURVE ( 'NONE', #8679, #18055, #6735, .T. ) ;
#6601=ORIENTED_EDGE ( 'NONE', *, *, #2906, .F. ) ;
#6615=CYLINDRICAL_SURFACE ( 'NONE', #3735, 21.00000000000008171 ) ;
#6618=CARTESIAN_POINT ( 'NONE',  ( -22.97163508793729036, -1.317345109681407722, 9.935299231138023046 ) ) ;
#6630=CARTESIAN_POINT ( 'NONE',  ( 0.000000000000000000, 0.000000000000000000, 77.51594804401857175 ) ) ;
#6636=EDGE_CURVE ( 'NONE', #580, #19076, #22144, .T. ) ;
#6640=CIRCLE ( 'NONE', #13097, 3.000000000000002665 ) ;
#6644=FACE_OUTER_BOUND ( 'NONE', #536, .T. ) ;
#6657=ORIENTED_EDGE ( 'NONE', *, *, #3842, .T. ) ;
#6661=AXIS2_PLACEMENT_3D ( 'NONE', #17893, #2456, #9666 ) ;
#6671=EDGE_CURVE ( 'NONE', #14415, #12719, #7072, .T. ) ;
#6677=AXIS2_PLACEMENT_3D ( 'NONE', #18028, #16226, #2707 ) ;
#6687=CARTESIAN_POINT ( 'NONE',  ( 0.000000000000000000, 22.63401512838754570, 77.51594804401857175 ) ) ;
#6690=AXIS2_PLACEMENT_3D ( 'NONE', #9135, #1210, #574 ) ;
#6724=CARTESIAN_POINT ( 'NONE',  ( 0.000000000000000000, 0.000000000000000000, 77.51594804401857175 ) ) ;
#6735=LINE ( 'NONE', #18770, #11723 ) ;
#6736=CARTESIAN_POINT ( 'NONE',  ( -21.73931781725157464, -7.525425332153104385, 6.616964900418876638 ) ) ;
#6759=DIRECTION ( 'NONE',  ( 0.000000000000000000, 0.000000000000000000, 1.000000000000000000 ) ) ;
#6781=ORIENTED_EDGE ( 'NONE', *, *, #12124, .T. ) ;
#6808=EDGE_LOOP ( 'NONE', ( #17981, #3578, #4262, #6142 ) ) ;
#6837=MANIFOLD_SOLID_BREP ( 'Mirror2', #8293 ) ;
#6842=LINE ( 'NONE', #11681, #9140 ) ;
#6845=CARTESIAN_POINT ( 'NONE',  ( -21.01246475424954596, -9.353905080905251523, 3.551468768066980530 ) ) ;
#6850=ORIENTED_EDGE ( 'NONE', *, *, #2389, .T. ) ;
#6857=EDGE_LOOP ( 'NONE', ( #794, #10365, #5711, #21919, #3704, #18021, #2327, #8058, #16491, #3166, #6781, #13498, #14756, #604, #16989, #13651, #2245, #9125, #12057, #10515, #278, #7371, #185, #1474, #5780, #13904 ) ) ;
#6882=EDGE_CURVE ( 'NONE', #1930, #2334, #15679, .T. ) ;
#6919=EDGE_LOOP ( 'NONE', ( #16239, #13346, #3996, #7526 ) ) ;
#6934=AXIS2_PLACEMENT_3D ( 'NONE', #18621, #12193, #10289 ) ;
#6935=VECTOR ( 'NONE', #19580, 1000.000000000000000 ) ;
#6944=CYLINDRICAL_SURFACE ( 'NONE', #14100, 23.00000000000008882 ) ;
#6959=CARTESIAN_POINT ( 'NONE',  ( -24.60211427235279302, 4.452209872279524916, 8.960190547743279055 ) ) ;
#6983=DIRECTION ( 'NONE',  ( 0.000000000000000000, 0.000000000000000000, -1.000000000000000000 ) ) ;
#6998=EDGE_CURVE ( 'NONE', #3746, #8392, #18554, .T. ) ;
#7029=AXIS2_PLACEMENT_3D ( 'NONE', #3784, #2098, #15618 ) ;
#7034=AXIS2_PLACEMENT_3D ( 'NONE', #20723, #6558, #5304 ) ;
#7044=LINE ( 'NONE', #11461, #15935 ) ;
#7072=LINE ( 'NONE', #5029, #16750 ) ;
#7084=ORIENTED_EDGE ( 'NONE', *, *, #6089, .T. ) ;
#7094=EDGE_CURVE ( 'NONE', #14027, #14742, #8853, .T. ) ;
#7121=EDGE_LOOP ( 'NONE', ( #2766, #19727, #6657, #17242 ) ) ;
#7146=ORIENTED_EDGE ( 'NONE', *, *, #19953, .T. ) ;
#7166=DIRECTION ( 'NONE',  ( -1.000000000000000000, 0.000000000000000000, 0.000000000000000000 ) ) ;
#7168=ADVANCED_FACE ( 'NONE', ( #3615 ), #15680, .T. ) ;
#7185=CARTESIAN_POINT ( 'NONE',  ( -23.33862492659004317, 8.963030688957390524, 4.446446727170273228 ) ) ;
#7205=EDGE_CURVE ( 'NONE', #19105, #324, #9148, .T. ) ;
#7211=DIRECTION ( 'NONE',  ( -1.000000000000000000, 0.000000000000000000, 0.000000000000000000 ) ) ;
#7220=ORIENTED_EDGE ( 'NONE', *, *, #14341, .T. ) ;
#7240=CARTESIAN_POINT ( 'NONE',  ( 0.000000000000000000, 0.000000000000000000, -75.00000000000000000 ) ) ;
#7273=VECTOR ( 'NONE', #1426, 1000.000000000000000 ) ;
#7296=CARTESIAN_POINT ( 'NONE',  ( -22.94872826613853434, 9.917518390247439086, 1.324323043557437574 ) ) ;
#7300=LINE ( 'NONE', #7624, #15934 ) ;
#7308=DIRECTION ( 'NONE',  ( -1.000000000000000000, 0.000000000000000000, 0.000000000000000000 ) ) ;
#7321=ADVANCED_FACE ( 'NONE', ( #12410 ), #16397, .T. ) ;
#7327=AXIS2_PLACEMENT_3D ( 'NONE', #19087, #5133, #18874 ) ;
#7333=VERTEX_POINT ( 'NONE', #17588 ) ;
#7340=LINE ( 'NONE', #3939, #7631 ) ;
#7354=DIRECTION ( 'NONE',  ( -1.000000000000000000, 0.000000000000000000, 0.000000000000000000 ) ) ;
#7371=ORIENTED_EDGE ( 'NONE', *, *, #14512, .T. ) ;
#7392=ORIENTED_EDGE ( 'NONE', *, *, #17196, .F. ) ;
#7397=TOROIDAL_SURFACE ( 'NONE', #9193, 22.63401512838748175, 3.000000000000002665 ) ;
#7404=DIRECTION ( 'NONE',  ( 0.000000000000000000, 0.000000000000000000, -1.000000000000000000 ) ) ;
#7405=CARTESIAN_POINT ( 'NONE',  ( -20.72032262650141021, 9.983465205454267632, 0.6641006075881642490 ) ) ;
#7442=ORIENTED_EDGE ( 'NONE', *, *, #12595, .F. ) ;
#7460=DIRECTION ( 'NONE',  ( 1.000000000000000000, 0.000000000000000000, 0.000000000000000000 ) ) ;
#7499=ORIENTED_EDGE ( 'NONE', *, *, #19590, .F. ) ;
#7512=CARTESIAN_POINT ( 'NONE',  ( -22.62231062914085555, 4.162462751021892338, -9.098484481344788932 ) ) ;
#7526=ORIENTED_EDGE ( 'NONE', *, *, #10754, .F. ) ;
#7529=ORIENTED_EDGE ( 'NONE', *, *, #21928, .T. ) ;
#7602=DIRECTION ( 'NONE',  ( 0.000000000000000000, 0.000000000000000000, 1.000000000000000000 ) ) ;
#7615=CARTESIAN_POINT ( 'NONE',  ( -25.00000000000013500, 1.972152263052529514E-28, -10.00000000000000000 ) ) ;
#7616=CARTESIAN_POINT ( 'NONE',  ( -20.71218630467650357, 10.00026692487615065, -0.6553852958034992460 ) ) ;
#7624=CARTESIAN_POINT ( 'NONE',  ( 0.000000000000000000, -23.00000000000006040, 75.00000000000000000 ) ) ;
#7631=VECTOR ( 'NONE', #10595, 1000.000000000000000 ) ;
#7633=FACE_OUTER_BOUND ( 'NONE', #16504, .T. ) ;
#7639=CARTESIAN_POINT ( 'NONE',  ( 0.000000000000000000, 0.000000000000000000, -55.00000000000000000 ) ) ;
#7642=AXIS2_PLACEMENT_3D ( 'NONE', #7894, #11483, #4275 ) ;
#7649=CARTESIAN_POINT ( 'NONE',  ( -22.77193774148174654, -3.246634745707170033, -9.464084820472235648 ) ) ;
#7650=CARTESIAN_POINT ( 'NONE',  ( 1.455845656607146304E-13, -21.63401512838760610, 77.51594804401857175 ) ) ;
#7672=TOROIDAL_SURFACE ( 'NONE', #10544, 22.63401512838748175, 3.000000000000002665 ) ;
#7681=SURFACE_STYLE_USAGE ( .BOTH. , #9807 ) ;
#7690=CYLINDRICAL_SURFACE ( 'NONE', #812, 23.00000000000008882 ) ;
#7697=EDGE_LOOP ( 'NONE', ( #14595, #15005, #8240, #5447 ) ) ;
#7706=CIRCLE ( 'NONE', #20618, 23.00000000000008882 ) ;
#7716=ORIENTED_EDGE ( 'NONE', *, *, #10506, .T. ) ;
#7722=TOROIDAL_SURFACE ( 'NONE', #20274, 22.63401512838748175, 3.000000000000002665 ) ;
#7727=CARTESIAN_POINT ( 'NONE',  ( -24.79573179333883814, -3.246809539008099765, 9.480629939678795637 ) ) ;
#7744=DIRECTION ( 'NONE',  ( -1.000000000000000000, 0.000000000000000000, 0.000000000000000000 ) ) ;
#7745=AXIS2_PLACEMENT_3D ( 'NONE', #18581, #6759, #15209 ) ;
#7746=ORIENTED_EDGE ( 'NONE', *, *, #6499, .F. ) ;
#7752=DIRECTION ( 'NONE',  ( 0.000000000000000000, 0.000000000000000000, -1.000000000000000000 ) ) ;
#7762=CARTESIAN_POINT ( 'NONE',  ( 0.000000000000000000, 0.000000000000000000, -55.00000000000000000 ) ) ;
#7826=DIRECTION ( 'NONE',  ( 0.000000000000000000, 0.000000000000000000, 1.000000000000000000 ) ) ;
#7827=DIRECTION ( 'NONE',  ( 0.000000000000000000, 0.000000000000000000, 1.000000000000000000 ) ) ;
#7838=CARTESIAN_POINT ( 'NONE',  ( -23.64367708099848286, -8.124846974203675742, 5.838821279329883041 ) ) ;
#7866=DIRECTION ( 'NONE',  ( 0.000000000000000000, 0.000000000000000000, 1.000000000000000000 ) ) ;
#7868=CIRCLE ( 'NONE', #1031, 3.000000000000002665 ) ;
#7894=CARTESIAN_POINT ( 'NONE',  ( 1.387778780781446180E-13, -19.80000000000006111, 78.50000000000000000 ) ) ;
#7909=PLANE ( 'NONE',  #15572 ) ;
#7932=DIRECTION ( 'NONE',  ( 0.000000000000000000, 0.000000000000000000, -1.000000000000000000 ) ) ;
#7933=DIRECTION ( 'NONE',  ( -1.000000000000000000, 0.000000000000000000, 0.000000000000000000 ) ) ;
#7945=CARTESIAN_POINT ( 'NONE',  ( -24.43287304230177881, -5.302030092552175056, 8.484947782864898258 ) ) ;
#7946=DIRECTION ( 'NONE',  ( -1.000000000000000000, 0.000000000000000000, 0.000000000000000000 ) ) ;
#7961=DIRECTION ( 'NONE',  ( 0.000000000000000000, 0.000000000000000000, -1.000000000000000000 ) ) ;
#7965=FACE_OUTER_BOUND ( 'NONE', #21141, .T. ) ;
#7971=AXIS2_PLACEMENT_3D ( 'NONE', #4312, #7932, #11195 ) ;
#8010=EDGE_CURVE ( 'NONE', #16287, #1838, #3672, .T. ) ;
#8011=AXIS2_PLACEMENT_3D ( 'NONE', #18224, #14521, #2784 ) ;
#8023=AXIS2_PLACEMENT_3D ( 'NONE', #16, #18596, #3268 ) ;
#8025=AXIS2_PLACEMENT_3D ( 'NONE', #19180, #4200, #16041 ) ;
#8058=ORIENTED_EDGE ( 'NONE', *, *, #14312, .F. ) ;
#8070=DIRECTION ( 'NONE',  ( 0.000000000000000000, 0.000000000000000000, -1.000000000000000000 ) ) ;
#8073=ORIENTED_EDGE ( 'NONE', *, *, #4247, .F. ) ;
#8079=ORIENTED_EDGE ( 'NONE', *, *, #2038, .T. ) ;
#8089=CARTESIAN_POINT ( 'NONE',  ( -24.49404684541703148, 5.034397176345765779, -8.664472460534662801 ) ) ;
#8094=CARTESIAN_POINT ( 'NONE',  ( -22.44689861640829776, -5.022254798600712000, 8.653524191425493228 ) ) ;
#8125=( NAMED_UNIT ( * ) PLANE_ANGLE_UNIT ( ) SI_UNIT ( $, .RADIAN. ) );
#8142=ORIENTED_EDGE ( 'NONE', *, *, #6998, .F. ) ;
#8170=CARTESIAN_POINT ( 'NONE',  ( -23.70956031934304775, -7.931217015752231703, 6.099360975250686323 ) ) ;
#8171=CARTESIAN_POINT ( 'NONE',  ( -22.63401512838757057, 0.000000000000000000, 77.51594804401857175 ) ) ;
#8200=DIRECTION ( 'NONE',  ( -1.000000000000000000, 0.000000000000000000, 0.000000000000000000 ) ) ;
#8203=CARTESIAN_POINT ( 'NONE',  ( -21.17929482144447206, -8.972977884236303936, 4.463132373296485156 ) ) ;
#8213=CARTESIAN_POINT ( 'NONE',  ( 0.000000000000000000, 21.00000000000006395, -75.00000000000000000 ) ) ;
#8227=CARTESIAN_POINT ( 'NONE',  ( -17.50000000000000711, 0.000000000000000000, -60.00000000000000000 ) ) ;
#8239=VECTOR ( 'NONE', #12142, 1000.000000000000000 ) ;
#8240=ORIENTED_EDGE ( 'NONE', *, *, #17580, .T. ) ;
#8267=CARTESIAN_POINT ( 'NONE',  ( 0.000000000000000000, 21.80000000000006111, -78.50000000000000000 ) ) ;
#8278=CARTESIAN_POINT ( 'NONE',  ( 1.526556658859590496E-13, -21.00000000000006040, 69.99999999999998579 ) ) ;
#8293=CLOSED_SHELL ( 'NONE', ( #4281, #17400, #9023, #10388, #20959, #20724, #13621, #10942, #19162, #1674, #14116, #3200, #10864, #4722, #18157, #10902, #22071, #21479, #5657, #11348, #5185, #19917, #9339, #15353, #18839, #5011, #9822, #7168, #8748, #3034, #21, #8972, #19678, #1033, #15864, #9155, #19715, #16574, #7321, #2121, #13110, #10313, #12571, #14783, #18288, #19004 ) ) ;
#8296=VERTEX_POINT ( 'NONE', #425 ) ;
#8330=EDGE_CURVE ( 'NONE', #3682, #19581, #239, .T. ) ;
#8338=CARTESIAN_POINT ( 'NONE',  ( -21.00000000000008171, 0.000000000000000000, -60.00000000000001421 ) ) ;
#8374=PRODUCT_DEFINITION ( 'UNKNOWN', '', #12463, #14834 ) ;
#8392=VERTEX_POINT ( 'NONE', #3902 ) ;
#8407=VERTEX_POINT ( 'NONE', #3791 ) ;
#8412=CARTESIAN_POINT ( 'NONE',  ( -23.00000000000000000, 0.000000000000000000, -30.00000000000000000 ) ) ;
#8422=EDGE_CURVE ( 'NONE', #19105, #14415, #20344, .T. ) ;
#8453=CARTESIAN_POINT ( 'NONE',  ( 1.665334536937735316E-13, -24.63401512838760610, -77.51594804401857175 ) ) ;
#8457=CARTESIAN_POINT ( 'NONE',  ( 0.000000000000000000, 0.000000000000000000, 75.00000000000000000 ) ) ;
#8469=ORIENTED_EDGE ( 'NONE', *, *, #12730, .T. ) ;
#8474=CIRCLE ( 'NONE', #1271, 19.80000000000007887 ) ;
#8526=VERTEX_POINT ( 'NONE', #9317 ) ;
#8543=CARTESIAN_POINT ( 'NONE',  ( -20.74454492543941342, -9.934009332729857533, -1.323381102396829379 ) ) ;
#8587=EDGE_CURVE ( 'NONE', #18055, #9712, #7300, .T. ) ;
#8590=VERTEX_POINT ( 'NONE', #14170 ) ;
#8643=CARTESIAN_POINT ( 'NONE',  ( -21.73559549195910634, 7.536301886650155879, 6.604919831454106216 ) ) ;
#8647=CARTESIAN_POINT ( 'NONE',  ( -24.79589088527667684, 3.246309046422540590, 9.481087457883008440 ) ) ;
#8657=DIRECTION ( 'NONE',  ( 1.000000000000000000, 0.000000000000000000, 0.000000000000000000 ) ) ;
#8658=ORIENTED_EDGE ( 'NONE', *, *, #21602, .T. ) ;
#8669=DIRECTION ( 'NONE',  ( -0.000000000000000000, 0.000000000000000000, -1.000000000000000000 ) ) ;
#8679=VERTEX_POINT ( 'NONE', #2211 ) ;
#8684=CARTESIAN_POINT ( 'NONE',  ( 0.000000000000000000, 21.00000000000006040, 69.99999999999998579 ) ) ;
#8689=EDGE_CURVE ( 'NONE', #16045, #11119, #2956, .T. ) ;
#8748=ADVANCED_FACE ( 'NONE', ( #14713 ), #19752, .F. ) ;
#8756=VECTOR ( 'NONE', #14483, 1000.000000000000000 ) ;
#8762=CARTESIAN_POINT ( 'NONE',  ( -24.96744712291844337, 1.317343280566261265, 9.918382748296247442 ) ) ;
#8768=ORIENTED_EDGE ( 'NONE', *, *, #20103, .T. ) ;
#8774=CARTESIAN_POINT ( 'NONE',  ( -23.00000000000000000, 0.000000000000000000, -24.99999999999999645 ) ) ;
#8775=VECTOR ( 'NONE', #11451, 1000.000000000000000 ) ;
#8776=ORIENTED_EDGE ( 'NONE', *, *, #22191, .F. ) ;
#8788=CARTESIAN_POINT ( 'NONE',  ( 0.000000000000000000, 0.000000000000000000, -24.99999999999999645 ) ) ;
#8810=ORIENTED_EDGE ( 'NONE', *, *, #15067, .T. ) ;
#8839=DIRECTION ( 'NONE',  ( -1.000000000000000000, 0.000000000000000000, 0.000000000000000000 ) ) ;
#8853=CIRCLE ( 'NONE', #21400, 21.00000000000008171 ) ;
#8854=DIRECTION ( 'NONE',  ( 1.401298464324817071E-45, 6.938893903907257960E-16, 1.000000000000000000 ) ) ;
#8860=CARTESIAN_POINT ( 'NONE',  ( -1.232595164407830946E-29, 17.50000000000007105, -24.99999999999999645 ) ) ;
#8868=DIRECTION ( 'NONE',  ( 0.000000000000000000, 0.000000000000000000, 1.000000000000000000 ) ) ;
#8873=VECTOR ( 'NONE', #9920, 1000.000000000000000 ) ;
#8940=EDGE_CURVE ( 'NONE', #2515, #3746, #19853, .T. ) ;
#8949=DIRECTION ( 'NONE',  ( -1.000000000000000000, 0.000000000000000000, 0.000000000000000000 ) ) ;
#8964=DIRECTION ( 'NONE',  ( 0.000000000000000000, 0.000000000000000000, -1.000000000000000000 ) ) ;
#8972=ADVANCED_FACE ( 'NONE', ( #6474 ), #3093, .F. ) ;
#8977=CARTESIAN_POINT ( 'NONE',  ( -25.00000000000013500, 6.609496070381316956E-17, -10.00000000000000000 ) ) ;
#8978=CARTESIAN_POINT ( 'NONE',  ( -23.00000000000000355, 0.3295946125619286238, 10.00000000000000000 ) ) ;
#8989=ORIENTED_EDGE ( 'NONE', *, *, #22191, .T. ) ;
#9012=EDGE_LOOP ( 'NONE', ( #12937, #11784, #5188, #3525, #14348, #14255 ) ) ;
#9022=DIRECTION ( 'NONE',  ( -0.000000000000000000, 0.000000000000000000, -1.000000000000000000 ) ) ;
#9023=ADVANCED_FACE ( 'NONE', ( #3182 ), #3330, .F. ) ;
#9036=DIRECTION ( 'NONE',  ( -1.000000000000000000, 0.000000000000000000, 0.000000000000000000 ) ) ;
#9055=CARTESIAN_POINT ( 'NONE',  ( -24.63401512838757768, 0.000000000000000000, -77.51594804401857175 ) ) ;
#9072=ORIENTED_EDGE ( 'NONE', *, *, #14496, .T. ) ;
#9087=CIRCLE ( 'NONE', #15213, 3.000000000000002665 ) ;
#9093=DIRECTION ( 'NONE',  ( -0.000000000000000000, -0.000000000000000000, -1.000000000000000000 ) ) ;
#9116=CARTESIAN_POINT ( 'NONE',  ( 0.000000000000000000, 0.000000000000000000, 78.50000000000000000 ) ) ;
#9125=ORIENTED_EDGE ( 'NONE', *, *, #6671, .F. ) ;
#9135=CARTESIAN_POINT ( 'NONE',  ( 0.000000000000000000, 0.000000000000000000, -55.00000000000000000 ) ) ;
#9140=VECTOR ( 'NONE', #20548, 1000.000000000000000 ) ;
#9143=EDGE_CURVE ( 'NONE', #15940, #3760, #9087, .T. ) ;
#9148=LINE ( 'NONE', #17478, #929 ) ;
#9155=ADVANCED_FACE ( 'NONE', ( #13781 ), #20619, .T. ) ;
#9157=CIRCLE ( 'NONE', #21355, 25.00000000000010303 ) ;
#9167=VERTEX_POINT ( 'NONE', #153 ) ;
#9170=ORIENTED_EDGE ( 'NONE', *, *, #15073, .T. ) ;
#9172=AXIS2_PLACEMENT_3D ( 'NONE', #1582, #1793, #18467 ) ;
#9193=AXIS2_PLACEMENT_3D ( 'NONE', #717, #3869, #17615 ) ;
#9197=ORIENTED_EDGE ( 'NONE', *, *, #3764, .F. ) ;
#9200=DIRECTION ( 'NONE',  ( 0.000000000000000000, 0.000000000000000000, -1.000000000000000000 ) ) ;
#9205=DIRECTION ( 'NONE',  ( 0.000000000000000000, 0.000000000000000000, -1.000000000000000000 ) ) ;
#9209=DIRECTION ( 'NONE',  ( 1.000000000000000000, 0.000000000000000000, 0.000000000000000000 ) ) ;
#9224=UNCERTAINTY_MEASURE_WITH_UNIT (LENGTH_MEASURE( 1.000000000000000082E-05 ), #16556, 'distance_accuracy_value', 'NONE');
#9240=ORIENTED_EDGE ( 'NONE', *, *, #8330, .F. ) ;
#9317=CARTESIAN_POINT ( 'NONE',  ( 0.000000000000000000, 23.00000000000006040, -30.00000000000000000 ) ) ;
#9325=DIRECTION ( 'NONE',  ( 0.000000000000000000, 0.000000000000000000, -1.000000000000000000 ) ) ;
#9338=CARTESIAN_POINT ( 'NONE',  ( -22.44874942423953357, -5.036274748608448704, -8.663716403940144417 ) ) ;
#9339=ADVANCED_FACE ( 'NONE', ( #21170 ), #7690, .F. ) ;
#9340=DIRECTION ( 'NONE',  ( 1.000000000000000000, 0.000000000000000000, 0.000000000000000000 ) ) ;
#9382=DIRECTION ( 'NONE',  ( 0.000000000000000000, 0.000000000000000000, -1.000000000000000000 ) ) ;
#9399=VERTEX_POINT ( 'NONE', #15909 ) ;
#9410=CARTESIAN_POINT ( 'NONE',  ( -23.45095836310901660, -8.671879559401306281, -5.022568673106638570 ) ) ;
#9428=CIRCLE ( 'NONE', #4730, 21.00000000000008527 ) ;
#9438=DIRECTION ( 'NONE',  ( 0.000000000000000000, 0.000000000000000000, -1.000000000000000000 ) ) ;
#9442=CIRCLE ( 'NONE', #20570, 23.00000000000008882 ) ;
#9447=APPLICATION_CONTEXT ( 'automotive_design' ) ;
#9449=DIRECTION ( 'NONE',  ( -0.000000000000000000, 0.000000000000000000, -1.000000000000000000 ) ) ;
#9456=ORIENTED_EDGE ( 'NONE', *, *, #11837, .T. ) ;
#9503=VECTOR ( 'NONE', #16942, 1000.000000000000000 ) ;
#9526=CARTESIAN_POINT ( 'NONE',  ( -24.60661961089613925, -4.459629237831038928, -8.974440426817473337 ) ) ;
#9534=DIRECTION ( 'NONE',  ( -1.000000000000000000, 0.000000000000000000, 0.000000000000000000 ) ) ;
#9542=DIRECTION ( 'NONE',  ( 0.000000000000000000, -1.000000000000000000, 0.000000000000000000 ) ) ;
#9560=DIRECTION ( 'NONE',  ( -1.000000000000000000, 0.000000000000000000, 0.000000000000000000 ) ) ;
#9561=FACE_OUTER_BOUND ( 'NONE', #16075, .T. ) ;
#9576=CIRCLE ( 'NONE', #21778, 21.63401512838748175 ) ;
#9620=DIRECTION ( 'NONE',  ( 0.000000000000000000, 0.000000000000000000, -1.000000000000000000 ) ) ;
#9633=CARTESIAN_POINT ( 'NONE',  ( -20.77601883660645754, 9.867231145063747988, 1.657240493860027586 ) ) ;
#9649=DIRECTION ( 'NONE',  ( 0.000000000000000000, 0.000000000000000000, -1.000000000000000000 ) ) ;
#9650=EDGE_LOOP ( 'NONE', ( #1714, #1082, #11835, #13011 ) ) ;
#9656=UNCERTAINTY_MEASURE_WITH_UNIT (LENGTH_MEASURE( 1.000000000000000082E-05 ), #18358, 'distance_accuracy_value', 'NONE');
#9666=DIRECTION ( 'NONE',  ( -1.000000000000000000, 0.000000000000000000, 0.000000000000000000 ) ) ;
#9712=VERTEX_POINT ( 'NONE', #1258 ) ;
#9731=CARTESIAN_POINT ( 'NONE',  ( -23.00000000000006750, -1.237926774615798086E-16, -10.00000000000000000 ) ) ;
#9740=CARTESIAN_POINT ( 'NONE',  ( -22.96972983264640078, -9.868964564168473785, 1.646689664842678091 ) ) ;
#9755=DIRECTION ( 'NONE',  ( -0.000000000000000000, 0.000000000000000000, -1.000000000000000000 ) ) ;
#9785=AXIS2_PLACEMENT_3D ( 'NONE', #18289, #19956, #6014 ) ;
#9798=DIRECTION ( 'NONE',  ( 1.000000000000000000, 0.000000000000000000, 0.000000000000000000 ) ) ;
#9805=VECTOR ( 'NONE', #14870, 1000.000000000000000 ) ;
#9807=SURFACE_SIDE_STYLE ('',( #20029 ) ) ;
#9815=DIRECTION ( 'NONE',  ( 0.000000000000000000, 0.000000000000000000, -1.000000000000000000 ) ) ;
#9820=VECTOR ( 'NONE', #9449, 1000.000000000000000 ) ;
#9822=ADVANCED_FACE ( 'NONE', ( #1035 ), #7909, .T. ) ;
#9851=VERTEX_POINT ( 'NONE', #14772 ) ;
#9854=DIRECTION ( 'NONE',  ( -1.000000000000000000, 0.000000000000000000, 0.000000000000000000 ) ) ;
#9876=LINE ( 'NONE', #16741, #8775 ) ;
#9920=DIRECTION ( 'NONE',  ( 4.408728476930457445E-15, -1.000000000000000000, 0.000000000000000000 ) ) ;
#9929=CIRCLE ( 'NONE', #12804, 25.00000000000010303 ) ;
#9941=VERTEX_POINT ( 'NONE', #18036 ) ;
#9965=EDGE_LOOP ( 'NONE', ( #21314, #15274, #11175, #16368 ) ) ;
#9997=CARTESIAN_POINT ( 'NONE',  ( -24.11388480999612938, 6.602120135752692853, -7.517827584289036302 ) ) ;
#9999=CARTESIAN_POINT ( 'NONE',  ( 0.000000000000000000, 23.00000000000006040, -69.99999999999998579 ) ) ;
#10018=VECTOR ( 'NONE', #2190, 1000.000000000000000 ) ;
#10027=CARTESIAN_POINT ( 'NONE',  ( -21.00000000000008171, 0.000000000000000000, 60.00000000000001421 ) ) ;
#10037=AXIS2_PLACEMENT_3D ( 'NONE', #4569, #9755, #14721 ) ;
#10038=EDGE_LOOP ( 'NONE', ( #6263, #8079, #9240, #13116 ) ) ;
#10092=CARTESIAN_POINT ( 'NONE',  ( -24.63401512838757768, 0.000000000000000000, -77.51594804401857175 ) ) ;
#10094=EDGE_CURVE ( 'NONE', #3236, #12201, #22040, .T. ) ;
#10099=LINE ( 'NONE', #11556, #5151 ) ;
#10116=VERTEX_POINT ( 'NONE', #18921 ) ;
#10136=PRODUCT ( 'top housing_top housing', 'top housing_top housing', '', ( #2638 ) ) ;
#10152=CIRCLE ( 'NONE', #13020, 23.00000000000008882 ) ;
#10160=ORIENTED_EDGE ( 'NONE', *, *, #14391, .F. ) ;
#10187=CYLINDRICAL_SURFACE ( 'NONE', #17434, 21.00000000000008171 ) ;
#10193=CIRCLE ( 'NONE', #17391, 21.80000000000008598 ) ;
#10222=CARTESIAN_POINT ( 'NONE',  ( -20.87479324910686529, -9.656827299161456324, -2.618089337444236442 ) ) ;
#10245=CARTESIAN_POINT ( 'NONE',  ( -25.00000000000013500, 1.224646799147555402E-15, 10.00000000000000000 ) ) ;
#10257=ORIENTED_EDGE ( 'NONE', *, *, #18574, .F. ) ;
#10264=EDGE_CURVE ( 'NONE', #19076, #13087, #21299, .T. ) ;
#10267=FACE_OUTER_BOUND ( 'NONE', #2769, .T. ) ;
#10280=CIRCLE ( 'NONE', #4510, 17.50000000000007816 ) ;
#10289=DIRECTION ( 'NONE',  ( -1.000000000000000000, 0.000000000000000000, 0.000000000000000000 ) ) ;
#10313=ADVANCED_FACE ( 'NONE', ( #5291 ), #20594, .T. ) ;
#10321=FACE_OUTER_BOUND ( 'NONE', #4817, .T. ) ;
#10330=CARTESIAN_POINT ( 'NONE',  ( -22.17595030361380637, 6.106954805067214664, 7.925275210824247907 ) ) ;
#10334=CARTESIAN_POINT ( 'NONE',  ( -20.77537792095403546, -9.868577331483782800, 1.649091285295470444 ) ) ;
#10365=ORIENTED_EDGE ( 'NONE', *, *, #16077, .F. ) ;
#10372=AXIS2_PLACEMENT_3D ( 'NONE', #16482, #7602, #6232 ) ;
#10388=ADVANCED_FACE ( 'NONE', ( #10267 ), #19876, .T. ) ;
#10397=CARTESIAN_POINT ( 'NONE',  ( 0.000000000000000000, 0.000000000000000000, -30.00000000000000000 ) ) ;
#10438=CARTESIAN_POINT ( 'NONE',  ( 1.232595164407830946E-29, -17.50000000000007105, -55.00000000000000000 ) ) ;
#10443=CARTESIAN_POINT ( 'NONE',  ( -22.97017636999641255, 9.867926576900321933, 1.652878766021345758 ) ) ;
#10487=ORIENTED_EDGE ( 'NONE', *, *, #20644, .T. ) ;
#10503=DIRECTION ( 'NONE',  ( 0.000000000000000000, 0.000000000000000000, 1.000000000000000000 ) ) ;
#10506=EDGE_CURVE ( 'NONE', #20995, #351, #18812, .T. ) ;
#10515=ORIENTED_EDGE ( 'NONE', *, *, #2798, .T. ) ;
#10534=LINE ( 'NONE', #6117, #13242 ) ;
#10544=AXIS2_PLACEMENT_3D ( 'NONE', #5397, #9438, #13981 ) ;
#10545=VERTEX_POINT ( 'NONE', #15446 ) ;
#10550=CARTESIAN_POINT ( 'NONE',  ( -22.03215468537991839, 6.606953063173292229, 7.513524830561480350 ) ) ;
#10565=DIRECTION ( 'NONE',  ( 0.000000000000000000, 0.000000000000000000, 1.000000000000000000 ) ) ;
#10566=VERTEX_POINT ( 'NONE', #16904 ) ;
#10575=DIRECTION ( 'NONE',  ( -1.000000000000000000, 0.000000000000000000, 0.000000000000000000 ) ) ;
#10578=CARTESIAN_POINT ( 'NONE',  ( 0.000000000000000000, 19.63401512838754215, 77.51594804401857175 ) ) ;
#10586=VERTEX_POINT ( 'NONE', #8684 ) ;
#10595=DIRECTION ( 'NONE',  ( 6.982962677686272233E-15, -1.000000000000000000, 0.000000000000000000 ) ) ;
#10597=VECTOR ( 'NONE', #3972, 1000.000000000000000 ) ;
#10608=DIRECTION ( 'NONE',  ( 0.000000000000000000, 0.000000000000000000, 1.000000000000000000 ) ) ;
#10619=CARTESIAN_POINT ( 'NONE',  ( 0.000000000000000000, 0.000000000000000000, 75.00000000000000000 ) ) ;
#10630=AXIS2_PLACEMENT_3D ( 'NONE', #1050, #21628, #6220 ) ;
#10635=CARTESIAN_POINT ( 'NONE',  ( 0.000000000000000000, 22.63401512838754570, 77.51594804401857175 ) ) ;
#10650=MECHANICAL_DESIGN_GEOMETRIC_PRESENTATION_REPRESENTATION('',(#13170),#18199);
#10651=CARTESIAN_POINT ( 'NONE',  ( -19.63401512838757057, -1.925929944387226885E-29, 77.51594804401857175 ) ) ;
#10653=AXIS2_PLACEMENT_3D ( 'NONE', #19150, #17698, #588 ) ;
#10665=LINE ( 'NONE', #17530, #4797 ) ;
#10666=FACE_OUTER_BOUND ( 'NONE', #12207, .T. ) ;
#10671=CARTESIAN_POINT ( 'NONE',  ( -23.05909213503509392, 9.658626557025268511, -2.611256163095958982 ) ) ;
#10675=DIRECTION ( 'NONE',  ( -1.000000000000000000, -6.982962677686272233E-15, 0.000000000000000000 ) ) ;
#10678=VERTEX_POINT ( 'NONE', #19659 ) ;
#10684=DIRECTION ( 'NONE',  ( -1.000000000000000000, 0.000000000000000000, 0.000000000000000000 ) ) ;
#10722=DIRECTION ( 'NONE',  ( -1.000000000000000000, 0.000000000000000000, 0.000000000000000000 ) ) ;
#10754=EDGE_CURVE ( 'NONE', #18119, #580, #12703, .T. ) ;
#10771=CARTESIAN_POINT ( 'NONE',  ( -23.00000000000000000, -1.421401133463427911E-20, 10.00000000000000000 ) ) ;
#10785=EDGE_LOOP ( 'NONE', ( #13954, #13523, #11446, #19220 ) ) ;
#10796=CARTESIAN_POINT ( 'NONE',  ( -21.63401512838757768, 0.000000000000000000, 77.51594804401857175 ) ) ;
#10814=DIRECTION ( 'NONE',  ( 0.000000000000000000, 0.000000000000000000, -1.000000000000000000 ) ) ;
#10827=CARTESIAN_POINT ( 'NONE',  ( 0.000000000000000000, 0.000000000000000000, 75.00000000000000000 ) ) ;
#10845=DIRECTION ( 'NONE',  ( 4.845403715540905824E-30, -6.938893903907257960E-16, -1.000000000000000000 ) ) ;
#10852=FACE_OUTER_BOUND ( 'NONE', #6919, .T. ) ;
#10862=LINE ( 'NONE', #12336, #2105 ) ;
#10864=ADVANCED_FACE ( 'NONE', ( #246 ), #7672, .T. ) ;
#10887=VERTEX_POINT ( 'NONE', #16191 ) ;
#10902=ADVANCED_FACE ( 'NONE', ( #763 ), #20819, .F. ) ;
#10909=CARTESIAN_POINT ( 'NONE',  ( 0.000000000000000000, 0.000000000000000000, -77.51594804401857175 ) ) ;
#10914=EDGE_CURVE ( 'NONE', #3468, #8526, #13416, .T. ) ;
#10918=ORIENTED_EDGE ( 'NONE', *, *, #9143, .T. ) ;
#10942=ADVANCED_FACE ( 'NONE', ( #3713 ), #14867, .F. ) ;
#10948=CIRCLE ( 'NONE', #169, 3.000000000000002665 ) ;
#10980=ORIENTED_EDGE ( 'NONE', *, *, #16436, .T. ) ;
#10984=AXIS2_PLACEMENT_3D ( 'NONE', #8788, #15650, #19445 ) ;
#11003=DIRECTION ( 'NONE',  ( 0.000000000000000000, 0.000000000000000000, 1.000000000000000000 ) ) ;
#11012=DIRECTION ( 'NONE',  ( 1.000000000000000000, 0.000000000000000000, 0.000000000000000000 ) ) ;
#11027=FACE_OUTER_BOUND ( 'NONE', #623, .T. ) ;
#11036=EDGE_CURVE ( 'NONE', #16801, #13087, #10099, .T. ) ;
#11072=CARTESIAN_POINT ( 'NONE',  ( 1.526556658859590748E-13, -21.00000000000006395, -75.00000000000000000 ) ) ;
#11089=DIRECTION ( 'NONE',  ( 0.000000000000000000, 0.000000000000000000, -1.000000000000000000 ) ) ;
#11102=CARTESIAN_POINT ( 'NONE',  ( -21.17702599587410717, 8.978242263026027459, -4.451669607260716255 ) ) ;
#11113=ORIENTED_EDGE ( 'NONE', *, *, #11545, .F. ) ;
#11118=DIRECTION ( 'NONE',  ( 0.000000000000000000, -1.000000000000000000, 0.000000000000000000 ) ) ;
#11119=VERTEX_POINT ( 'NONE', #15168 ) ;
#11132=LINE ( 'NONE', #2890, #4492 ) ;
#11133=DIRECTION ( 'NONE',  ( -1.000000000000000000, 0.000000000000000000, 0.000000000000000000 ) ) ;
#11142=CARTESIAN_POINT ( 'NONE',  ( -21.63401512838757768, 0.000000000000000000, -77.51594804401857175 ) ) ;
#11175=ORIENTED_EDGE ( 'NONE', *, *, #19320, .T. ) ;
#11193=EDGE_CURVE ( 'NONE', #12695, #12719, #9876, .T. ) ;
#11195=DIRECTION ( 'NONE',  ( -1.000000000000000000, 0.000000000000000000, 0.000000000000000000 ) ) ;
#11202=VECTOR ( 'NONE', #9022, 1000.000000000000000 ) ;
#11208=CARTESIAN_POINT ( 'NONE',  ( -23.00000000000007105, 0.3345464022992510333, -10.00000000000000000 ) ) ;
#11211=DIRECTION ( 'NONE',  ( -1.000000000000000000, 0.000000000000000000, 0.000000000000000000 ) ) ;
#11213=CIRCLE ( 'NONE', #1505, 21.00000000000008171 ) ;
#11219=ORIENTED_EDGE ( 'NONE', *, *, #1722, .T. ) ;
#11233=TOROIDAL_SURFACE ( 'NONE', #11586, 24.63401512838747820, 3.000000000000000888 ) ;
#11239=CARTESIAN_POINT ( 'NONE',  ( -23.00000000000006750, -1.237926774615798086E-16, -10.00000000000000000 ) ) ;
#11240=LINE ( 'NONE', #16423, #18435 ) ;
#11248=ORIENTED_EDGE ( 'NONE', *, *, #16821, .T. ) ;
#11279=VECTOR ( 'NONE', #1690, 1000.000000000000000 ) ;
#11280=DIRECTION ( 'NONE',  ( 1.000000000000000000, 4.408728476930457445E-15, 0.000000000000000000 ) ) ;
#11297=CIRCLE ( 'NONE', #21696, 21.00000000000008527 ) ;
#11315=ORIENTED_EDGE ( 'NONE', *, *, #22048, .T. ) ;
#11341=DIRECTION ( 'NONE',  ( -0.000000000000000000, 0.000000000000000000, -1.000000000000000000 ) ) ;
#11348=ADVANCED_FACE ( 'NONE', ( #20315 ), #4910, .F. ) ;
#11353=EDGE_CURVE ( 'NONE', #20454, #9399, #17746, .T. ) ;
#11378=CARTESIAN_POINT ( 'NONE',  ( 1.232595164407830946E-29, -17.50000000000007105, -55.00000000000000000 ) ) ;
#11392=DIRECTION ( 'NONE',  ( -1.000000000000000000, 0.000000000000000000, 0.000000000000000000 ) ) ;
#11400=ORIENTED_EDGE ( 'NONE', *, *, #17132, .F. ) ;
#11416=DIRECTION ( 'NONE',  ( 0.000000000000000000, 0.000000000000000000, 1.000000000000000000 ) ) ;
#11428=CARTESIAN_POINT ( 'NONE',  ( -24.99350385409967856, -0.6578573476328165581, 9.983793171540982669 ) ) ;
#11446=ORIENTED_EDGE ( 'NONE', *, *, #13649, .T. ) ;
#11451=DIRECTION ( 'NONE',  ( 0.000000000000000000, 0.000000000000000000, -1.000000000000000000 ) ) ;
#11455=CARTESIAN_POINT ( 'NONE',  ( -23.18379035723104664, 9.355751749453526500, -3.546302055531801223 ) ) ;
#11461=CARTESIAN_POINT ( 'NONE',  ( 0.000000000000000000, 23.00000000000006040, 69.99999999999998579 ) ) ;
#11483=DIRECTION ( 'NONE',  ( 0.000000000000000000, 0.000000000000000000, 1.000000000000000000 ) ) ;
#11484=DIRECTION ( 'NONE',  ( -0.000000000000000000, -1.000000000000000000, -0.000000000000000000 ) ) ;
#11506=ORIENTED_EDGE ( 'NONE', *, *, #12730, .F. ) ;
#11533=CARTESIAN_POINT ( 'NONE',  ( -24.96757326990382708, -1.314646799225510199, 9.918699822820977730 ) ) ;
#11545=EDGE_CURVE ( 'NONE', #12391, #15108, #18795, .T. ) ;
#11551=ORIENTED_EDGE ( 'NONE', *, *, #440, .T. ) ;
#11554=DIRECTION ( 'NONE',  ( -1.000000000000000000, 0.000000000000000000, 0.000000000000000000 ) ) ;
#11556=CARTESIAN_POINT ( 'NONE',  ( 2.465190328815661892E-29, 25.00000000000012790, -75.00000000000000000 ) ) ;
#11561=CARTESIAN_POINT ( 'NONE',  ( -23.84293592645385473, 7.532792288779332601, -6.608927698841862153 ) ) ;
#11566=DIRECTION ( 'NONE',  ( 0.000000000000000000, 0.000000000000000000, -1.000000000000000000 ) ) ;
#11579=AXIS2_PLACEMENT_3D ( 'NONE', #17290, #21098, #2195 ) ;
#11585=EDGE_CURVE ( 'NONE', #20364, #16045, #5868, .T. ) ;
#11586=AXIS2_PLACEMENT_3D ( 'NONE', #19118, #5274, #343 ) ;
#11618=ORIENTED_EDGE ( 'NONE', *, *, #15930, .F. ) ;
#11632=AXIS2_PLACEMENT_3D ( 'NONE', #15497, #20538, #17410 ) ;
#11636=CARTESIAN_POINT ( 'NONE',  ( 0.000000000000000000, -23.00000000000006040, -69.99999999999998579 ) ) ;
#11647=CARTESIAN_POINT ( 'NONE',  ( -23.05940187647296469, -9.657892124444725113, -2.614105026375423524 ) ) ;
#11665=EDGE_LOOP ( 'NONE', ( #6850, #1043, #2191, #21088, #736, #19983 ) ) ;
#11679=CARTESIAN_POINT ( 'NONE',  ( -23.28348052659234924, 9.104820739214817493, -4.148323561781968927 ) ) ;
#11681=CARTESIAN_POINT ( 'NONE',  ( 0.000000000000000000, 23.00000000000006040, 75.00000000000000000 ) ) ;
#11684=CARTESIAN_POINT ( 'NONE',  ( -20.96199077856121207, -9.466050238387317961, 3.240634028981310255 ) ) ;
#11688=CIRCLE ( 'NONE', #7745, 17.50000000000007816 ) ;
#11710=DIRECTION ( 'NONE',  ( -6.982962677686272233E-15, 1.000000000000000000, 0.000000000000000000 ) ) ;
#11721=ORIENTED_EDGE ( 'NONE', *, *, #13389, .F. ) ;
#11723=VECTOR ( 'NONE', #1667, 1000.000000000000000 ) ;
#11725=VECTOR ( 'NONE', #4616, 1000.000000000000000 ) ;
#11758=EDGE_CURVE ( 'NONE', #21649, #14946, #20800, .T. ) ;
#11784=ORIENTED_EDGE ( 'NONE', *, *, #13717, .F. ) ;
#11789=CARTESIAN_POINT ( 'NONE',  ( 0.000000000000000000, 0.000000000000000000, 75.00000000000000000 ) ) ;
#11800=CARTESIAN_POINT ( 'NONE',  ( -22.03409719845232928, -6.612754814632006095, 7.529125094242241190 ) ) ;
#11804=VERTEX_POINT ( 'NONE', #10796 ) ;
#11816=AXIS2_PLACEMENT_3D ( 'NONE', #17286, #5453, #7166 ) ;
#11835=ORIENTED_EDGE ( 'NONE', *, *, #16439, .F. ) ;
#11837=EDGE_CURVE ( 'NONE', #10545, #5175, #844, .T. ) ;
#11869=ORIENTED_EDGE ( 'NONE', *, *, #11193, .F. ) ;
#11893=CARTESIAN_POINT ( 'NONE',  ( 1.232595164407830946E-29, -17.50000000000007105, -60.00000000000000000 ) ) ;
#11906=CARTESIAN_POINT ( 'NONE',  ( -22.62392499481471120, -4.153411067053860428, 9.102477892503269885 ) ) ;
#11912=ORIENTED_EDGE ( 'NONE', *, *, #925, .T. ) ;
#12021=CARTESIAN_POINT ( 'NONE',  ( -20.96318929043787449, -9.463403270074600471, -3.248492544644434599 ) ) ;
#12057=ORIENTED_EDGE ( 'NONE', *, *, #19702, .T. ) ;
#12070=ORIENTED_EDGE ( 'NONE', *, *, #4685, .F. ) ;
#12086=DIRECTION ( 'NONE',  ( -1.000000000000000000, 0.000000000000000000, 0.000000000000000000 ) ) ;
#12089=AXIS2_PLACEMENT_3D ( 'NONE', #20550, #5249, #22145 ) ;
#12124=EDGE_CURVE ( 'NONE', #8392, #20174, #994, .T. ) ;
#12127=CARTESIAN_POINT ( 'NONE',  ( -21.12229863832016008, 9.103146205856329942, 4.151976327957419777 ) ) ;
#12131=CARTESIAN_POINT ( 'NONE',  ( -24.49077085807447318, 5.028751554214830222, 8.649788737574644060 ) ) ;
#12142=DIRECTION ( 'NONE',  ( -1.083936797661037871E-15, -1.000000000000000000, 0.000000000000000000 ) ) ;
#12193=DIRECTION ( 'NONE',  ( 0.000000000000000000, 0.000000000000000000, -1.000000000000000000 ) ) ;
#12201=VERTEX_POINT ( 'NONE', #19995 ) ;
#12207=EDGE_LOOP ( 'NONE', ( #17976, #12661, #3676, #3299 ) ) ;
#12223=CARTESIAN_POINT ( 'NONE',  ( -1.232595164407830946E-29, 17.50000000000007105, -24.99999999999999645 ) ) ;
#12224=ORIENTED_EDGE ( 'NONE', *, *, #21373, .F. ) ;
#12233=ORIENTED_EDGE ( 'NONE', *, *, #21602, .F. ) ;
#12236=CARTESIAN_POINT ( 'NONE',  ( -2.465190328815661892E-29, -25.00000000000012790, -75.00000000000000000 ) ) ;
#12237=CARTESIAN_POINT ( 'NONE',  ( -22.99291885829180515, 0.6598326085037610200, 9.983746764812034158 ) ) ;
#12241=CARTESIAN_POINT ( 'NONE',  ( -22.91284222278097360, 10.00008306376378364, -0.6577592246564750722 ) ) ;
#12261=CARTESIAN_POINT ( 'NONE',  ( 0.000000000000000000, 0.000000000000000000, -69.99999999999998579 ) ) ;
#12273=ORIENTED_EDGE ( 'NONE', *, *, #2906, .T. ) ;
#12281=CARTESIAN_POINT ( 'NONE',  ( 0.000000000000000000, 0.000000000000000000, -30.00000000000000000 ) ) ;
#12299=CIRCLE ( 'NONE', #1866, 17.50000000000007816 ) ;
#12331=TOROIDAL_SURFACE ( 'NONE', #8025, 24.63401512838747820, 3.000000000000000888 ) ;
#12336=CARTESIAN_POINT ( 'NONE',  ( 0.000000000000000000, -23.00000000000006040, 75.00000000000000000 ) ) ;
#12337=DIRECTION ( 'NONE',  ( -1.000000000000000000, 0.000000000000000000, 0.000000000000000000 ) ) ;
#12351=CIRCLE ( 'NONE', #16300, 3.000000000000002665 ) ;
#12352=CARTESIAN_POINT ( 'NONE',  ( -1.232595164407830946E-29, 17.50000000000007105, -24.99999999999999645 ) ) ;
#12389=ORIENTED_EDGE ( 'NONE', *, *, #8587, .T. ) ;
#12391=VERTEX_POINT ( 'NONE', #19772 ) ;
#12410=FACE_OUTER_BOUND ( 'NONE', #20453, .T. ) ;
#12431=AXIS2_PLACEMENT_3D ( 'NONE', #693, #2156, #5645 ) ;
#12463=PRODUCT_DEFINITION_FORMATION_WITH_SPECIFIED_SOURCE ( 'ANY', '', #10136, .NOT_KNOWN. ) ;
#12465=ORIENTED_EDGE ( 'NONE', *, *, #18879, .T. ) ;
#12468=CARTESIAN_POINT ( 'NONE',  ( -24.89698496326684207, -2.290081829390879342, -9.739783964571683939 ) ) ;
#12472=( NAMED_UNIT ( * ) PLANE_ANGLE_UNIT ( ) SI_UNIT ( $, .RADIAN. ) );
#12522=DIRECTION ( 'NONE',  ( -0.000000000000000000, 0.000000000000000000, -1.000000000000000000 ) ) ;
#12571=ADVANCED_FACE ( 'NONE', ( #1328 ), #6615, .F. ) ;
#12572=CARTESIAN_POINT ( 'NONE',  ( -22.38029933203972277, 5.310221276841376792, -8.479724577993932755 ) ) ;
#12595=EDGE_CURVE ( 'NONE', #16686, #3236, #15614, .T. ) ;
#12643=EDGE_CURVE ( 'NONE', #8526, #21835, #6842, .T. ) ;
#12649=CARTESIAN_POINT ( 'NONE',  ( -20.99999999999999645, 0.000000000000000000, 69.99999999999998579 ) ) ;
#12661=ORIENTED_EDGE ( 'NONE', *, *, #11585, .T. ) ;
#12680=CARTESIAN_POINT ( 'NONE',  ( -22.77746302204332451, 3.250740792401631829, -9.479807400168150266 ) ) ;
#12691=ORIENTED_EDGE ( 'NONE', *, *, #16077, .T. ) ;
#12695=VERTEX_POINT ( 'NONE', #20438 ) ;
#12697=CYLINDRICAL_SURFACE ( 'NONE', #21868, 10.00000000000000000 ) ;
#12698=ORIENTED_EDGE ( 'NONE', *, *, #4652, .F. ) ;
#12703=CIRCLE ( 'NONE', #1567, 21.80000000000008598 ) ;
#12712=DIRECTION ( 'NONE',  ( -0.000000000000000000, 0.000000000000000000, -1.000000000000000000 ) ) ;
#12719=VERTEX_POINT ( 'NONE', #20210 ) ;
#12730=EDGE_CURVE ( 'NONE', #351, #324, #7706, .T. ) ;
#12736=LINE ( 'NONE', #11378, #6935 ) ;
#12767=CARTESIAN_POINT ( 'NONE',  ( 0.000000000000000000, 0.000000000000000000, -75.00000000000000000 ) ) ;
#12788=ORIENTED_EDGE ( 'NONE', *, *, #6538, .T. ) ;
#12792=CARTESIAN_POINT ( 'NONE',  ( -20.95684706105100759, 9.480813542266940175, -3.246593753853921349 ) ) ;
#12795=SURFACE_STYLE_USAGE ( .BOTH. , #2101 ) ;
#12804=AXIS2_PLACEMENT_3D ( 'NONE', #7240, #12522, #9036 ) ;
#12824=CARTESIAN_POINT ( 'NONE',  ( -23.00000000000007461, -0.6697502447017975591, -10.00000000000000000 ) ) ;
#12825=DIRECTION ( 'NONE',  ( 0.000000000000000000, 0.000000000000000000, -1.000000000000000000 ) ) ;
#12832=EDGE_LOOP ( 'NONE', ( #20894, #17316, #3595, #651, #3378, #4676 ) ) ;
#12877=ORIENTED_EDGE ( 'NONE', *, *, #19590, .T. ) ;
#12882=FACE_OUTER_BOUND ( 'NONE', #6242, .T. ) ;
#12893=VERTEX_POINT ( 'NONE', #9999 ) ;
#12897=CARTESIAN_POINT ( 'NONE',  ( -22.44443515611089168, 5.033198366023263759, -8.647132211342501762 ) ) ;
#12912=VERTEX_POINT ( 'NONE', #1664 ) ;
#12923=CARTESIAN_POINT ( 'NONE',  ( 2.465190328815661892E-29, 24.63401512838760610, 77.51594804401857175 ) ) ;
#12930=CARTESIAN_POINT ( 'NONE',  ( 1.232595164407830946E-29, -17.50000000000007105, -55.00000000000000000 ) ) ;
#12937=ORIENTED_EDGE ( 'NONE', *, *, #16303, .F. ) ;
#12952=LINE ( 'NONE', #21262, #21268 ) ;
#12996=EDGE_CURVE ( 'NONE', #3760, #20454, #5135, .T. ) ;
#12998=AXIS2_PLACEMENT_3D ( 'NONE', #16483, #13217, #19952 ) ;
#13003=CARTESIAN_POINT ( 'NONE',  ( -21.80000000000008242, 0.000000000000000000, -78.50000000000000000 ) ) ;
#13004=CARTESIAN_POINT ( 'NONE',  ( -20.75208159527516472, 9.917280711861716114, 1.325952641556472189 ) ) ;
#13011=ORIENTED_EDGE ( 'NONE', *, *, #17601, .F. ) ;
#13013=DIRECTION ( 'NONE',  ( 0.000000000000000000, 0.000000000000000000, 1.000000000000000000 ) ) ;
#13020=AXIS2_PLACEMENT_3D ( 'NONE', #15996, #16438, #16213 ) ;
#13033=AXIS2_PLACEMENT_3D ( 'NONE', #7762, #4147, #11133 ) ;
#13034=CARTESIAN_POINT ( 'NONE',  ( -24.79131200319441319, 3.238905045468998267, -9.466624808433273586 ) ) ;
#13047=EDGE_LOOP ( 'NONE', ( #5342, #10980, #9197, #15838 ) ) ;
#13087=VERTEX_POINT ( 'NONE', #14164 ) ;
#13097=AXIS2_PLACEMENT_3D ( 'NONE', #10635, #22221, #1742 ) ;
#13105=DIRECTION ( 'NONE',  ( -2.162300680179986877E-16, -1.000000000000000000, 0.000000000000000000 ) ) ;
#13110=ADVANCED_FACE ( 'NONE', ( #10666 ), #18484, .F. ) ;
#13116=ORIENTED_EDGE ( 'NONE', *, *, #16303, .T. ) ;
#13119=CARTESIAN_POINT ( 'NONE',  ( -23.02481977093860621, -9.739746005238293591, -2.290462534298830288 ) ) ;
#13137=VECTOR ( 'NONE', #19558, 1000.000000000000000 ) ;
#13142=CARTESIAN_POINT ( 'NONE',  ( 0.000000000000000000, 0.000000000000000000, 75.00000000000000000 ) ) ;
#13147=CARTESIAN_POINT ( 'NONE',  ( -24.74863962610228185, 3.549617057581722968, -9.354628607790802519 ) ) ;
#13170=STYLED_ITEM ( 'NONE', ( #19641 ), #6837 ) ;
#13192=CARTESIAN_POINT ( 'NONE',  ( 0.000000000000000000, -23.00000000000006040, 75.00000000000000000 ) ) ;
#13199=EDGE_CURVE ( 'NONE', #15746, #10887, #15665, .T. ) ;
#13217=DIRECTION ( 'NONE',  ( 0.000000000000000000, 0.000000000000000000, 1.000000000000000000 ) ) ;
#13238=EDGE_CURVE ( 'NONE', #15108, #6126, #4753, .T. ) ;
#13242=VECTOR ( 'NONE', #13105, 1000.000000000000000 ) ;
#13244=EDGE_LOOP ( 'NONE', ( #15492, #12465, #2440, #20565 ) ) ;
#13256=CIRCLE ( 'NONE', #2471, 17.50000000000007816 ) ;
#13260=CARTESIAN_POINT ( 'NONE',  ( -23.00000000000000000, -1.421401133463427911E-20, 10.00000000000000000 ) ) ;
#13284=DIRECTION ( 'NONE',  ( 0.000000000000000000, 0.000000000000000000, 1.000000000000000000 ) ) ;
#13290=PRESENTATION_STYLE_ASSIGNMENT (( #7681 ) ) ;
#13335=CARTESIAN_POINT ( 'NONE',  ( -23.33508647570782557, -8.974881619392299115, 4.459489333929378851 ) ) ;
#13346=ORIENTED_EDGE ( 'NONE', *, *, #19894, .T. ) ;
#13364=AXIS2_PLACEMENT_3D ( 'NONE', #17956, #836, #2631 ) ;
#13381=CARTESIAN_POINT ( 'NONE',  ( 0.000000000000000000, -23.00000000000006040, -24.99999999999999645 ) ) ;
#13387=VECTOR ( 'NONE', #4948, 1000.000000000000000 ) ;
#13389=EDGE_CURVE ( 'NONE', #4564, #645, #11297, .T. ) ;
#13416=CIRCLE ( 'NONE', #6586, 23.00000000000008882 ) ;
#13421=ORIENTED_EDGE ( 'NONE', *, *, #2389, .F. ) ;
#13436=AXIS2_PLACEMENT_3D ( 'NONE', #12261, #3691, #10575 ) ;
#13453=CIRCLE ( 'NONE', #13822, 19.80000000000007887 ) ;
#13468=DIRECTION ( 'NONE',  ( -0.000000000000000000, -0.000000000000000000, -1.000000000000000000 ) ) ;
#13482=DIRECTION ( 'NONE',  ( 0.000000000000000000, 0.000000000000000000, 1.000000000000000000 ) ) ;
#13484=CARTESIAN_POINT ( 'NONE',  ( 0.000000000000000000, 0.000000000000000000, -69.99999999999998579 ) ) ;
#13488=CARTESIAN_POINT ( 'NONE',  ( -20.71220452560666203, -10.00022918515372794, 0.3239426289883403642 ) ) ;
#13494=AXIS2_PLACEMENT_3D ( 'NONE', #1384, #20495, #17250 ) ;
#13498=ORIENTED_EDGE ( 'NONE', *, *, #4247, .T. ) ;
#13500=DIRECTION ( 'NONE',  ( 0.000000000000000000, 0.000000000000000000, 1.000000000000000000 ) ) ;
#13502=ORIENTED_EDGE ( 'NONE', *, *, #16439, .T. ) ;
#13514=CARTESIAN_POINT ( 'NONE',  ( 1.665334536937735820E-13, -23.00000000000006040, -69.99999999999998579 ) ) ;
#13523=ORIENTED_EDGE ( 'NONE', *, *, #598, .T. ) ;
#13532=CARTESIAN_POINT ( 'NONE',  ( 1.665334536937735820E-13, -23.00000000000006040, 69.99999999999998579 ) ) ;
#13591=LINE ( 'NONE', #11893, #7273 ) ;
#13615=FACE_OUTER_BOUND ( 'NONE', #12832, .T. ) ;
#13621=ADVANCED_FACE ( 'NONE', ( #3304 ), #1944, .T. ) ;
#13630=PLANE ( 'NONE',  #5115 ) ;
#13649=EDGE_CURVE ( 'NONE', #3862, #8296, #20257, .T. ) ;
#13651=ORIENTED_EDGE ( 'NONE', *, *, #3080, .T. ) ;
#13678=DIRECTION ( 'NONE',  ( -0.000000000000000000, 0.000000000000000000, -1.000000000000000000 ) ) ;
#13692=EDGE_CURVE ( 'NONE', #7333, #3760, #13453, .T. ) ;
#13708=CARTESIAN_POINT ( 'NONE',  ( 1.526556658859591000E-13, -22.63401512838754570, 77.51594804401857175 ) ) ;
#13709=DIRECTION ( 'NONE',  ( -1.000000000000000000, 0.000000000000000000, 0.000000000000000000 ) ) ;
#13710=DIRECTION ( 'NONE',  ( -1.000000000000000000, 0.000000000000000000, 0.000000000000000000 ) ) ;
#13717=EDGE_CURVE ( 'NONE', #9167, #3682, #3086, .T. ) ;
#13781=FACE_OUTER_BOUND ( 'NONE', #11665, .T. ) ;
#13792=CARTESIAN_POINT ( 'NONE',  ( 0.000000000000000000, 0.000000000000000000, 60.00000000000001421 ) ) ;
#13822=AXIS2_PLACEMENT_3D ( 'NONE', #20178, #18737, #7946 ) ;
#13831=CARTESIAN_POINT ( 'NONE',  ( -23.51643582902884333, 8.486085053562996805, 5.300072969598608630 ) ) ;
#13851=DIRECTION ( 'NONE',  ( 0.000000000000000000, 0.000000000000000000, -1.000000000000000000 ) ) ;
#13856=CARTESIAN_POINT ( 'NONE',  ( -19.80000000000007532, 0.000000000000000000, -78.50000000000000000 ) ) ;
#13871=CARTESIAN_POINT ( 'NONE',  ( 0.000000000000000000, 0.000000000000000000, -77.51594804401857175 ) ) ;
#13883=CIRCLE ( 'NONE', #6690, 17.50000000000007816 ) ;
#13885=CIRCLE ( 'NONE', #5964, 25.00000000000010303 ) ;
#13904=ORIENTED_EDGE ( 'NONE', *, *, #10264, .T. ) ;
#13910=ORIENTED_EDGE ( 'NONE', *, *, #4050, .F. ) ;
#13942=CARTESIAN_POINT ( 'NONE',  ( -22.91289665287838773, 9.999958348741847303, 0.3307720414079513560 ) ) ;
#13954=ORIENTED_EDGE ( 'NONE', *, *, #14312, .T. ) ;
#13971=ORIENTED_EDGE ( 'NONE', *, *, #18479, .F. ) ;
#13979=AXIS2_PLACEMENT_3D ( 'NONE', #2768, #9649, #7744 ) ;
#13981=DIRECTION ( 'NONE',  ( -1.000000000000000000, 0.000000000000000000, 0.000000000000000000 ) ) ;
#13996=FACE_OUTER_BOUND ( 'NONE', #9650, .T. ) ;
#14027=VERTEX_POINT ( 'NONE', #8278 ) ;
#14036=LINE ( 'NONE', #8860, #16562 ) ;
#14047=DIRECTION ( 'NONE',  ( 0.000000000000000000, 0.000000000000000000, -1.000000000000000000 ) ) ;
#14091=DIRECTION ( 'NONE',  ( 0.000000000000000000, 0.000000000000000000, -1.000000000000000000 ) ) ;
#14093=DIRECTION ( 'NONE',  ( -1.000000000000000000, 0.000000000000000000, 0.000000000000000000 ) ) ;
#14100=AXIS2_PLACEMENT_3D ( 'NONE', #18540, #20429, #17184 ) ;
#14112=AXIS2_PLACEMENT_3D ( 'NONE', #16432, #6172, #6399 ) ;
#14116=ADVANCED_FACE ( 'NONE', ( #19286 ), #10187, .F. ) ;
#14122=VECTOR ( 'NONE', #2349, 1000.000000000000000 ) ;
#14142=AXIS2_PLACEMENT_3D ( 'NONE', #2324, #9093, #9209 ) ;
#14164=CARTESIAN_POINT ( 'NONE',  ( 0.000000000000000000, 23.00000000000006395, -75.00000000000000000 ) ) ;
#14170=CARTESIAN_POINT ( 'NONE',  ( -1.232595164407830946E-29, 17.50000000000007105, -30.00000000000000000 ) ) ;
#14233=EDGE_CURVE ( 'NONE', #16873, #16801, #9157, .T. ) ;
#14240=ORIENTED_EDGE ( 'NONE', *, *, #6382, .T. ) ;
#14243=ORIENTED_EDGE ( 'NONE', *, *, #18092, .F. ) ;
#14250=CARTESIAN_POINT ( 'NONE',  ( 0.000000000000000000, -23.00000000000006040, -60.00000000000000000 ) ) ;
#14255=ORIENTED_EDGE ( 'NONE', *, *, #17479, .F. ) ;
#14275=CARTESIAN_POINT ( 'NONE',  ( -21.95886157946472750, 6.845920284573796089, -7.296501936155945778 ) ) ;
#14302=CARTESIAN_POINT ( 'NONE',  ( 1.232595164407830946E-29, -17.50000000000007105, -24.99999999999999645 ) ) ;
#14312=EDGE_CURVE ( 'NONE', #16331, #15940, #6640, .T. ) ;
#14334=VECTOR ( 'NONE', #8854, 1000.000000000000000 ) ;
#14341=EDGE_CURVE ( 'NONE', #2064, #8296, #884, .T. ) ;
#14348=ORIENTED_EDGE ( 'NONE', *, *, #12996, .T. ) ;
#14351=DIRECTION ( 'NONE',  ( -1.000000000000000000, 0.000000000000000000, 0.000000000000000000 ) ) ;
#14379=CARTESIAN_POINT ( 'NONE',  ( -22.94233912960511645, 1.659357271331404871, -9.866832502321154053 ) ) ;
#14391=EDGE_CURVE ( 'NONE', #15638, #16686, #19496, .T. ) ;
#14409=LINE ( 'NONE', #2783, #13137 ) ;
#14410=DIRECTION ( 'NONE',  ( -0.000000000000000000, 0.000000000000000000, -1.000000000000000000 ) ) ;
#14415=VERTEX_POINT ( 'NONE', #19609 ) ;
#14454=AXIS2_PLACEMENT_3D ( 'NONE', #6453, #11416, #16590 ) ;
#14477=APPLICATION_CONTEXT ( 'automotive_design' ) ;
#14483=DIRECTION ( 'NONE',  ( 1.000000000000000000, 0.000000000000000000, 0.000000000000000000 ) ) ;
#14484=CARTESIAN_POINT ( 'NONE',  ( -20.74377437872641394, 9.935632711291296104, -1.314056478963706365 ) ) ;
#14487=AXIS2_PLACEMENT_3D ( 'NONE', #16394, #8070, #973 ) ;
#14496=EDGE_CURVE ( 'NONE', #1365, #15746, #19559, .T. ) ;
#14512=EDGE_CURVE ( 'NONE', #645, #9941, #10948, .T. ) ;
#14520=DIRECTION ( 'NONE',  ( 0.000000000000000000, 0.000000000000000000, 1.000000000000000000 ) ) ;
#14521=DIRECTION ( 'NONE',  ( 0.000000000000000000, 0.000000000000000000, -1.000000000000000000 ) ) ;
#14529=ORIENTED_EDGE ( 'NONE', *, *, #14233, .T. ) ;
#14537=CARTESIAN_POINT ( 'NONE',  ( 0.000000000000000000, 0.000000000000000000, 77.51594804401857175 ) ) ;
#14544=ORIENTED_EDGE ( 'NONE', *, *, #22017, .F. ) ;
#14557=VECTOR ( 'NONE', #10845, 1000.000000000000000 ) ;
#14571=CIRCLE ( 'NONE', #5210, 17.50000000000007816 ) ;
#14586=FACE_OUTER_BOUND ( 'NONE', #6005, .T. ) ;
#14595=ORIENTED_EDGE ( 'NONE', *, *, #12595, .T. ) ;
#14598=CARTESIAN_POINT ( 'NONE',  ( -23.13321191529080068, -9.483104312044424944, 3.241338891325622473 ) ) ;
#14610=ORIENTED_EDGE ( 'NONE', *, *, #3080, .F. ) ;
#14611=STYLED_ITEM ( 'NONE', ( #13290 ), #20620 ) ;
#14616=LINE ( 'NONE', #21671, #15069 ) ;
#14631=CARTESIAN_POINT ( 'NONE',  ( 0.000000000000000000, 0.000000000000000000, -24.99999999999999645 ) ) ;
#14642=SHAPE_REPRESENTATION ( 'top housing_top housing', ( #6677 ), #2013 ) ;
#14673=ORIENTED_EDGE ( 'NONE', *, *, #2939, .F. ) ;
#14704=CARTESIAN_POINT ( 'NONE',  ( -23.13924380385313739, -9.465003506282521073, -3.243783901925690216 ) ) ;
#14705=CARTESIAN_POINT ( 'NONE',  ( -20.86724456400193617, 9.673627921070774960, -2.620012337426697258 ) ) ;
#14711=EDGE_LOOP ( 'NONE', ( #2422, #18952, #18949, #18008, #8073, #14673 ) ) ;
#14713=FACE_OUTER_BOUND ( 'NONE', #17763, .T. ) ;
#14721=DIRECTION ( 'NONE',  ( -1.000000000000000000, 0.000000000000000000, 0.000000000000000000 ) ) ;
#14725=CYLINDRICAL_SURFACE ( 'NONE', #21616, 25.00000000000010303 ) ;
#14727=CARTESIAN_POINT ( 'NONE',  ( 0.000000000000000000, 0.000000000000000000, -78.50000000000000000 ) ) ;
#14730=CARTESIAN_POINT ( 'NONE',  ( 0.000000000000000000, 0.000000000000000000, 75.00000000000000000 ) ) ;
#14742=VERTEX_POINT ( 'NONE', #12649 ) ;
#14755=CARTESIAN_POINT ( 'NONE',  ( -1.232595164407830946E-29, 17.50000000000007105, -30.00000000000000000 ) ) ;
#14756=ORIENTED_EDGE ( 'NONE', *, *, #5761, .T. ) ;
#14763=LINE ( 'NONE', #2486, #11725 ) ;
#14770=EDGE_CURVE ( 'NONE', #16045, #17384, #18351, .T. ) ;
#14772=CARTESIAN_POINT ( 'NONE',  ( -25.00000000000013500, 6.609496070381316956E-17, -10.00000000000000000 ) ) ;
#14783=ADVANCED_FACE ( 'NONE', ( #21183 ), #7722, .T. ) ;
#14797=AXIS2_PLACEMENT_3D ( 'NONE', #18865, #20313, #15057 ) ;
#14806=EDGE_LOOP ( 'NONE', ( #281, #4899, #12698, #19018, #12224, #7442, #10160, #3743, #19184, #5704, #868, #20336, #18819, #21016, #1112, #2748, #13910, #22231, #17181, #5816, #8658, #4039, #15519, #99, #21103, #12788 ) ) ;
#14809=CARTESIAN_POINT ( 'NONE',  ( -25.00000000000000000, -1.002884296170500229E-19, 10.00000000000000000 ) ) ;
#14810=CARTESIAN_POINT ( 'NONE',  ( 1.387778780781446180E-13, -19.80000000000006111, 78.50000000000000000 ) ) ;
#14825=TOROIDAL_SURFACE ( 'NONE', #14112, 22.63401512838748175, 3.000000000000002665 ) ;
#14834=PRODUCT_DEFINITION_CONTEXT ( 'detailed design', #14477, 'design' ) ;
#14844=CARTESIAN_POINT ( 'NONE',  ( -22.03110473117843071, -6.610460937067380804, -7.510453512272658116 ) ) ;
#14845=PLANE ( 'NONE',  #2975 ) ;
#14867=TOROIDAL_SURFACE ( 'NONE', #4796, 24.63401512838747820, 3.000000000000000888 ) ;
#14869=TOROIDAL_SURFACE ( 'NONE', #7327, 22.63401512838748175, 3.000000000000002665 ) ;
#14870=DIRECTION ( 'NONE',  ( 0.000000000000000000, -1.000000000000000000, 0.000000000000000000 ) ) ;
#14893=EDGE_CURVE ( 'NONE', #1644, #11119, #2678, .T. ) ;
#14921=CIRCLE ( 'NONE', #9172, 21.00000000000008171 ) ;
#14927=CARTESIAN_POINT ( 'NONE',  ( -24.49265865991512214, -5.019550820411826209, 8.655126539049678769 ) ) ;
#14946=VERTEX_POINT ( 'NONE', #8227 ) ;
#14956=CARTESIAN_POINT ( 'NONE',  ( -24.89656853084665400, 2.294499589785194971, -9.738719574107680188 ) ) ;
#14961=CARTESIAN_POINT ( 'NONE',  ( -21.30902137360851967, -8.664601116739698128, 5.034284465761014182 ) ) ;
#14990=EDGE_CURVE ( 'NONE', #14742, #10586, #14921, .T. ) ;
#14991=( NAMED_UNIT ( * ) SI_UNIT ( $, .STERADIAN. ) SOLID_ANGLE_UNIT ( ) );
#15005=ORIENTED_EDGE ( 'NONE', *, *, #10094, .T. ) ;
#15024=CARTESIAN_POINT ( 'NONE',  ( -23.00000000000009237, 0.000000000000000000, 75.00000000000000000 ) ) ;
#15036=CARTESIAN_POINT ( 'NONE',  ( -23.91245210406065524, -7.297367535069414934, 6.844934202459222128 ) ) ;
#15057=DIRECTION ( 'NONE',  ( 0.000000000000000000, 0.000000000000000000, 1.000000000000000000 ) ) ;
#15066=CARTESIAN_POINT ( 'NONE',  ( -24.99323045272601007, 0.6685402709427104018, -9.983109981726205007 ) ) ;
#15067=EDGE_CURVE ( 'NONE', #10545, #4564, #5164, .T. ) ;
#15069=VECTOR ( 'NONE', #11118, 1000.000000000000000 ) ;
#15073=EDGE_CURVE ( 'NONE', #351, #15638, #15325, .T. ) ;
#15083=VERTEX_POINT ( 'NONE', #20126 ) ;
#15108=VERTEX_POINT ( 'NONE', #20352 ) ;
#15157=ORIENTED_EDGE ( 'NONE', *, *, #14233, .F. ) ;
#15168=CARTESIAN_POINT ( 'NONE',  ( -23.00000000000009237, 0.000000000000000000, -75.00000000000000000 ) ) ;
#15175=CIRCLE ( 'NONE', #14797, 3.000000000000002665 ) ;
#15182=DIRECTION ( 'NONE',  ( -1.000000000000000000, 0.000000000000000000, 0.000000000000000000 ) ) ;
#15183=CIRCLE ( 'NONE', #15904, 19.63401512838747820 ) ;
#15209=DIRECTION ( 'NONE',  ( -1.000000000000000000, 0.000000000000000000, 0.000000000000000000 ) ) ;
#15213=AXIS2_PLACEMENT_3D ( 'NONE', #6687, #39, #10503 ) ;
#15250=EDGE_CURVE ( 'NONE', #12719, #14946, #11688, .T. ) ;
#15252=FACE_OUTER_BOUND ( 'NONE', #9965, .T. ) ;
#15274=ORIENTED_EDGE ( 'NONE', *, *, #16032, .T. ) ;
#15285=AXIS2_PLACEMENT_3D ( 'NONE', #9055, #11484, #15922 ) ;
#15297=CARTESIAN_POINT ( 'NONE',  ( 0.000000000000000000, 0.000000000000000000, -60.00000000000001421 ) ) ;
#15310=DIRECTION ( 'NONE',  ( -1.000000000000000000, 0.000000000000000000, 0.000000000000000000 ) ) ;
#15325=LINE ( 'NONE', #13514, #21725 ) ;
#15353=ADVANCED_FACE ( 'NONE', ( #6644 ), #18904, .F. ) ;
#15374=CARTESIAN_POINT ( 'NONE',  ( 0.000000000000000000, 0.000000000000000000, -75.00000000000000000 ) ) ;
#15424=VECTOR ( 'NONE', #9542, 1000.000000000000000 ) ;
#15446=CARTESIAN_POINT ( 'NONE',  ( -20.99999999999999645, 0.000000000000000000, -69.99999999999998579 ) ) ;
#15480=B_SPLINE_CURVE_WITH_KNOTS ( 'NONE', 3,
 ( #8977, #20998, #15841, #12468, #3892, #17636, #4436, #9526, #18406, #18297, #4771, #16602, #21766, #4660, #18188, #9410, #1071, #20073, #14704, #11647, #13119, #2856, #19744, #2968, #4324, #16719, #9740, #21652, #14598, #13335, #18519, #7838, #8170, #19849, #15036, #16385, #850, #7945, #14927, #19965, #16274, #7727, #1296, #964, #11533, #11428, #6466, #14809 ),
 .UNSPECIFIED., .F., .F.,
 ( 4, 2, 2, 2, 2, 2, 2, 2, 2, 2, 2, 2, 2, 2, 2, 2, 2, 2, 2, 2, 2, 2, 2, 4 ),
 ( 6.413919134271389359E-20, 0.001974931581232642393, 0.002962397371848964241, 0.003949863162465286522, 0.005924794743697927614, 0.006912260534314250762, 0.007899726324930574778, 0.009874657906163219340, 0.01184958948739586564, 0.01283705527801219139, 0.01382452106862851540, 0.01579945264986116343, 0.01678691844047748571, 0.01777438423109381493, 0.01974931581232645950, 0.02172424739355911100, 0.02271171318417543675, 0.02369917897479175903, 0.02567411055602440706, 0.02666157634664072934, 0.02764904213725705509, 0.02962397371848970312, 0.03061143950910603234, 0.03159890529972235462 ),
 .UNSPECIFIED. ) ;
#15492=ORIENTED_EDGE ( 'NONE', *, *, #7094, .T. ) ;
#15497=CARTESIAN_POINT ( 'NONE',  ( 2.465190328815661892E-29, 24.63401512838760610, 77.51594804401857175 ) ) ;
#15499=B_SPLINE_CURVE_WITH_KNOTS ( 'NONE', 3,
 ( #2208, #1879, #3566, #8762, #17197, #1773, #8647, #2102, #6959, #12131, #316, #15622, #15846, #15738, #5474, #13831, #20667, #7185, #17303, #18986, #17423, #10443, #7296, #203, #13942, #12241, #19092, #1992, #10671, #4349, #11455, #11679, #4687, #19770, #21567, #1214, #11561, #4803, #9997, #18104, #3117, #8089, #4467, #13147, #13034, #19880, #14956, #1098, #6156, #15066, #21796, #1435 ),
 .UNSPECIFIED., .F., .F.,
 ( 4, 2, 2, 2, 2, 2, 2, 2, 2, 2, 2, 2, 2, 2, 2, 2, 2, 2, 2, 2, 2, 2, 2, 2, 2, 4 ),
 ( 0.03159890529972235462, 0.03258572303769623896, 0.03357254077567013023, 0.03554617625161789890, 0.03653299398959179017, 0.03751981172756567451, 0.03949344720351345706, 0.04146708267946123266, 0.04245390041743511700, 0.04344071815540900827, 0.04541435363135679082, 0.04640117136933068209, 0.04738798910730457337, 0.04936162458325235591, 0.05034844232122625413, 0.05133526005920014540, 0.05232207779717404361, 0.05330889553514793489, 0.05528253101109571743, 0.05626934874906960871, 0.05725616648704350692, 0.05922980196299128253, 0.06021661970096517380, 0.06120343743893906507, 0.06219025517691295635, 0.06317707291488684762 ),
 .UNSPECIFIED. ) ;
#15504=CARTESIAN_POINT ( 'NONE',  ( -21.37887586799824646, 8.484154883082068110, 5.303148973211635031 ) ) ;
#15513=ORIENTED_EDGE ( 'NONE', *, *, #6671, .T. ) ;
#15519=ORIENTED_EDGE ( 'NONE', *, *, #8330, .T. ) ;
#15565=CYLINDRICAL_SURFACE ( 'NONE', #7034, 25.00000000000010303 ) ;
#15572=AXIS2_PLACEMENT_3D ( 'NONE', #13192, #11280, #21394 ) ;
#15573=AXIS2_PLACEMENT_3D ( 'NONE', #19560, #9340, #16526 ) ;
#15614=CIRCLE ( 'NONE', #16735, 3.000000000000002665 ) ;
#15617=DIRECTION ( 'NONE',  ( -1.000000000000000000, 0.000000000000000000, 0.000000000000000000 ) ) ;
#15618=DIRECTION ( 'NONE',  ( -1.000000000000000000, 0.000000000000000000, 0.000000000000000000 ) ) ;
#15622=CARTESIAN_POINT ( 'NONE',  ( -24.24718929195449135, 6.113767028403175985, 7.939869996053141143 ) ) ;
#15637=LINE ( 'NONE', #17548, #8239 ) ;
#15638=VERTEX_POINT ( 'NONE', #16093 ) ;
#15650=DIRECTION ( 'NONE',  ( 0.000000000000000000, 0.000000000000000000, -1.000000000000000000 ) ) ;
#15665=CIRCLE ( 'NONE', #3013, 19.80000000000007887 ) ;
#15668=CARTESIAN_POINT ( 'NONE',  ( 0.000000000000000000, 0.000000000000000000, 77.51594804401857175 ) ) ;
#15679=CIRCLE ( 'NONE', #16050, 23.00000000000008882 ) ;
#15680=PLANE ( 'NONE',  #3453 ) ;
#15711=CARTESIAN_POINT ( 'NONE',  ( 0.000000000000000000, 23.00000000000006040, -24.99999999999999289 ) ) ;
#15720=DIRECTION ( 'NONE',  ( -0.000000000000000000, -1.000000000000000000, -0.000000000000000000 ) ) ;
#15730=EDGE_LOOP ( 'NONE', ( #5585, #14240, #7392, #7220 ) ) ;
#15737=SURFACE_STYLE_FILL_AREA ( #4118 ) ;
#15738=CARTESIAN_POINT ( 'NONE',  ( -23.84163028481813029, 7.537079486365330538, 6.604381661968267814 ) ) ;
#15746=VERTEX_POINT ( 'NONE', #13856 ) ;
#15838=ORIENTED_EDGE ( 'NONE', *, *, #17864, .F. ) ;
#15841=CARTESIAN_POINT ( 'NONE',  ( -24.97326975762673840, -1.324061100770212773, -9.933696595364846615 ) ) ;
#15842=CARTESIAN_POINT ( 'NONE',  ( -22.77738497769248127, 3.250935496930576818, 9.479599941460891799 ) ) ;
#15845=( LENGTH_UNIT ( ) NAMED_UNIT ( * ) SI_UNIT ( .MILLI., .METRE. ) );
#15846=CARTESIAN_POINT ( 'NONE',  ( -24.11365241543554916, 6.615335895425515034, 7.527466726025860311 ) ) ;
#15858=ORIENTED_EDGE ( 'NONE', *, *, #19516, .T. ) ;
#15864=ADVANCED_FACE ( 'NONE', ( #17665 ), #17328, .F. ) ;
#15904=AXIS2_PLACEMENT_3D ( 'NONE', #21584, #2899, #6065 ) ;
#15909=CARTESIAN_POINT ( 'NONE',  ( 2.465190328815681510E-29, 21.63401512838760610, 77.51594804401857175 ) ) ;
#15912=AXIS2_PLACEMENT_3D ( 'NONE', #19859, #18084, #9534 ) ;
#15919=ORIENTED_EDGE ( 'NONE', *, *, #22048, .F. ) ;
#15922=DIRECTION ( 'NONE',  ( 0.000000000000000000, 0.000000000000000000, -1.000000000000000000 ) ) ;
#15930=EDGE_CURVE ( 'NONE', #9167, #7333, #8474, .T. ) ;
#15934=VECTOR ( 'NONE', #21005, 1000.000000000000000 ) ;
#15935=VECTOR ( 'NONE', #18557, 1000.000000000000000 ) ;
#15940=VERTEX_POINT ( 'NONE', #10578 ) ;
#15956=( NAMED_UNIT ( * ) SI_UNIT ( $, .STERADIAN. ) SOLID_ANGLE_UNIT ( ) );
#15963=ORIENTED_EDGE ( 'NONE', *, *, #925, .F. ) ;
#15968=DIRECTION ( 'NONE',  ( 0.000000000000000000, 0.000000000000000000, -1.000000000000000000 ) ) ;
#15996=CARTESIAN_POINT ( 'NONE',  ( 0.000000000000000000, 0.000000000000000000, 75.00000000000000000 ) ) ;
#16032=EDGE_CURVE ( 'NONE', #18699, #18628, #14571, .T. ) ;
#16034=ORIENTED_EDGE ( 'NONE', *, *, #22184, .F. ) ;
#16041=DIRECTION ( 'NONE',  ( -1.000000000000000000, 0.000000000000000000, 0.000000000000000000 ) ) ;
#16045=VERTEX_POINT ( 'NONE', #21463 ) ;
#16050=AXIS2_PLACEMENT_3D ( 'NONE', #2319, #9205, #21216 ) ;
#16051=CARTESIAN_POINT ( 'NONE',  ( -21.00000000000000000, 0.000000000000000000, -75.00000000000000000 ) ) ;
#16075=EDGE_LOOP ( 'NONE', ( #16034, #13421, #12389, #12877 ) ) ;
#16077=EDGE_CURVE ( 'NONE', #17072, #16801, #11132, .T. ) ;
#16093=CARTESIAN_POINT ( 'NONE',  ( 1.526556658859590496E-13, -21.00000000000006040, -69.99999999999998579 ) ) ;
#16094=LINE ( 'NONE', #12930, #14122 ) ;
#16100=ORIENTED_EDGE ( 'NONE', *, *, #11353, .T. ) ;
#16113=PLANE ( 'NONE',  #7642 ) ;
#16124=CIRCLE ( 'NONE', #22235, 23.00000000000008882 ) ;
#16170=DIRECTION ( 'NONE',  ( 0.000000000000000000, 0.000000000000000000, -1.000000000000000000 ) ) ;
#16186=ORIENTED_EDGE ( 'NONE', *, *, #1896, .F. ) ;
#16191=CARTESIAN_POINT ( 'NONE',  ( 0.000000000000000000, 19.80000000000006111, -78.50000000000000000 ) ) ;
#16198=CARTESIAN_POINT ( 'NONE',  ( -21.81074228087361178, -7.304017576129684386, -6.837760653483515583 ) ) ;
#16213=DIRECTION ( 'NONE',  ( 1.000000000000000000, 0.000000000000000000, 0.000000000000000000 ) ) ;
#16219=LINE ( 'NONE', #14755, #9805 ) ;
#16226=DIRECTION ( 'NONE',  ( 0.000000000000000000, 0.000000000000000000, 1.000000000000000000 ) ) ;
#16239=ORIENTED_EDGE ( 'NONE', *, *, #3764, .T. ) ;
#16241=ORIENTED_EDGE ( 'NONE', *, *, #2466, .T. ) ;
#16261=CARTESIAN_POINT ( 'NONE',  ( 0.000000000000000000, 0.000000000000000000, -75.00000000000000000 ) ) ;
#16262=EDGE_CURVE ( 'NONE', #10887, #580, #14409, .T. ) ;
#16274=CARTESIAN_POINT ( 'NONE',  ( -24.65527973750573665, -4.148457894541834001, 9.104741959888016822 ) ) ;
#16275=CARTESIAN_POINT ( 'NONE',  ( -22.96373804598209389, 1.332909331808050490, -9.916358630100157612 ) ) ;
#16281=CIRCLE ( 'NONE', #15573, 3.000000000000002665 ) ;
#16287=VERTEX_POINT ( 'NONE', #883 ) ;
#16299=AXIS2_PLACEMENT_3D ( 'NONE', #7639, #7752, #17992 ) ;
#16300=AXIS2_PLACEMENT_3D ( 'NONE', #5588, #635, #7404 ) ;
#16303=EDGE_CURVE ( 'NONE', #3682, #8407, #5931, .T. ) ;
#16309=FACE_OUTER_BOUND ( 'NONE', #5283, .T. ) ;
#16331=VERTEX_POINT ( 'NONE', #21241 ) ;
#16338=( NAMED_UNIT ( * ) PLANE_ANGLE_UNIT ( ) SI_UNIT ( $, .RADIAN. ) );
#16359=CIRCLE ( 'NONE', #6661, 21.63401512838748175 ) ;
#16368=ORIENTED_EDGE ( 'NONE', *, *, #485, .F. ) ;
#16385=CARTESIAN_POINT ( 'NONE',  ( -24.11485229701111166, -6.610722576001652584, 7.531077992868392634 ) ) ;
#16389=CARTESIAN_POINT ( 'NONE',  ( 0.000000000000000000, 0.000000000000000000, 69.99999999999998579 ) ) ;
#16394=CARTESIAN_POINT ( 'NONE',  ( 0.000000000000000000, 0.000000000000000000, -55.00000000000000000 ) ) ;
#16397=TOROIDAL_SURFACE ( 'NONE', #19261, 22.63401512838748175, 3.000000000000002665 ) ;
#16398=ORIENTED_EDGE ( 'NONE', *, *, #10094, .F. ) ;
#16399=( GEOMETRIC_REPRESENTATION_CONTEXT ( 3 ) GLOBAL_UNCERTAINTY_ASSIGNED_CONTEXT ( ( #9224 ) ) GLOBAL_UNIT_ASSIGNED_CONTEXT ( ( #16556, #16338, #2597 ) ) REPRESENTATION_CONTEXT ( 'NONE', 'WORKASPACE' ) );
#16405=EDGE_LOOP ( 'NONE', ( #11551, #17730, #20964, #4860 ) ) ;
#16422=CARTESIAN_POINT ( 'NONE',  ( -22.88757527474730580, -2.294270667724057855, -9.738816109291027701 ) ) ;
#16423=CARTESIAN_POINT ( 'NONE',  ( -23.00000000000008882, 0.000000000000000000, 75.00000000000000000 ) ) ;
#16432=CARTESIAN_POINT ( 'NONE',  ( 0.000000000000000000, 0.000000000000000000, 77.51594804401857175 ) ) ;
#16436=EDGE_CURVE ( 'NONE', #20364, #1644, #16359, .T. ) ;
#16438=DIRECTION ( 'NONE',  ( -0.000000000000000000, -0.000000000000000000, -1.000000000000000000 ) ) ;
#16439=EDGE_CURVE ( 'NONE', #6126, #15108, #3407, .T. ) ;
#16453=CARTESIAN_POINT ( 'NONE',  ( 0.000000000000000000, 0.000000000000000000, -55.00000000000000000 ) ) ;
#16482=CARTESIAN_POINT ( 'NONE',  ( 0.000000000000000000, 0.000000000000000000, 77.51594804401857175 ) ) ;
#16483=CARTESIAN_POINT ( 'NONE',  ( 0.000000000000000000, 0.000000000000000000, -30.00000000000000000 ) ) ;
#16491=ORIENTED_EDGE ( 'NONE', *, *, #3842, .F. ) ;
#16504=EDGE_LOOP ( 'NONE', ( #19538, #2642, #10487, #6372 ) ) ;
#16525=CARTESIAN_POINT ( 'NONE',  ( -22.72510797543546346, -3.558559409777959370, -9.351142534105258974 ) ) ;
#16526=DIRECTION ( 'NONE',  ( 0.000000000000000000, 0.000000000000000000, -1.000000000000000000 ) ) ;
#16556=( LENGTH_UNIT ( ) NAMED_UNIT ( * ) SI_UNIT ( .MILLI., .METRE. ) );
#16562=VECTOR ( 'NONE', #20872, 1000.000000000000000 ) ;
#16570=EDGE_LOOP ( 'NONE', ( #19200, #510, #18536, #17951 ) ) ;
#16574=ADVANCED_FACE ( 'NONE', ( #1441 ), #4692, .F. ) ;
#16590=DIRECTION ( 'NONE',  ( 1.000000000000000000, 0.000000000000000000, 0.000000000000000000 ) ) ;
#16602=CARTESIAN_POINT ( 'NONE',  ( -24.11215523719795328, -6.608422274973745125, -7.512281027134874556 ) ) ;
#16603=DIRECTION ( 'NONE',  ( -1.000000000000000000, 0.000000000000000000, 0.000000000000000000 ) ) ;
#16608=AXIS2_PLACEMENT_3D ( 'NONE', #15668, #17467, #5181 ) ;
#16618=VECTOR ( 'NONE', #21921, 1000.000000000000000 ) ;
#16632=DIRECTION ( 'NONE',  ( -1.000000000000000000, 0.000000000000000000, 0.000000000000000000 ) ) ;
#16662=CIRCLE ( 'NONE', #21678, 3.000000000000002665 ) ;
#16681=AXIS2_PLACEMENT_3D ( 'NONE', #16720, #21989, #16603 ) ;
#16686=VERTEX_POINT ( 'NONE', #422 ) ;
#16716=ORIENTED_EDGE ( 'NONE', *, *, #198, .T. ) ;
#16719=CARTESIAN_POINT ( 'NONE',  ( -22.94848423520210901, -9.918082410655362224, 1.320023449481911415 ) ) ;
#16720=CARTESIAN_POINT ( 'NONE',  ( 0.000000000000000000, 0.000000000000000000, 77.51594804401857175 ) ) ;
#16735=AXIS2_PLACEMENT_3D ( 'NONE', #3001, #16862, #6384 ) ;
#16741=CARTESIAN_POINT ( 'NONE',  ( -1.232595164407830946E-29, 17.50000000000007105, -55.00000000000000000 ) ) ;
#16750=VECTOR ( 'NONE', #3667, 1000.000000000000000 ) ;
#16752=CIRCLE ( 'NONE', #12431, 3.000000000000002665 ) ;
#16790=ORIENTED_EDGE ( 'NONE', *, *, #18479, .T. ) ;
#16801=VERTEX_POINT ( 'NONE', #20886 ) ;
#16821=EDGE_CURVE ( 'NONE', #12391, #9851, #15499, .T. ) ;
#16844=CIRCLE ( 'NONE', #11816, 23.00000000000008882 ) ;
#16862=DIRECTION ( 'NONE',  ( -1.000000000000000000, -6.982962677686272233E-15, 0.000000000000000000 ) ) ;
#16873=VERTEX_POINT ( 'NONE', #6273 ) ;
#16904=CARTESIAN_POINT ( 'NONE',  ( 1.526556658859590496E-13, -21.80000000000006111, -78.50000000000000000 ) ) ;
#16929=LINE ( 'NONE', #1504, #20536 ) ;
#16942=DIRECTION ( 'NONE',  ( 6.982962677686272233E-15, -1.000000000000000000, 0.000000000000000000 ) ) ;
#16975=CARTESIAN_POINT ( 'NONE',  ( -23.00000000000000000, -0.6598369341251709708, 10.00000000000000178 ) ) ;
#16981=ORIENTED_EDGE ( 'NONE', *, *, #4047, .F. ) ;
#16989=ORIENTED_EDGE ( 'NONE', *, *, #12643, .T. ) ;
#16995=EDGE_CURVE ( 'NONE', #9399, #12912, #19877, .T. ) ;
#16998=EDGE_CURVE ( 'NONE', #8296, #16331, #5153, .T. ) ;
#17021=DIRECTION ( 'NONE',  ( 1.000000000000000000, 0.000000000000000000, 0.000000000000000000 ) ) ;
#17056=DIRECTION ( 'NONE',  ( -1.000000000000000000, 0.000000000000000000, 0.000000000000000000 ) ) ;
#17071=CARTESIAN_POINT ( 'NONE',  ( 0.000000000000000000, 0.000000000000000000, 75.00000000000000000 ) ) ;
#17072=VERTEX_POINT ( 'NONE', #6494 ) ;
#17132=EDGE_CURVE ( 'NONE', #19581, #16287, #4418, .T. ) ;
#17181=ORIENTED_EDGE ( 'NONE', *, *, #18365, .T. ) ;
#17184=DIRECTION ( 'NONE',  ( -1.000000000000000000, 0.000000000000000000, 0.000000000000000000 ) ) ;
#17192=CARTESIAN_POINT ( 'NONE',  ( -21.58783780880416003, 7.944440104776258949, 6.107615235951442401 ) ) ;
#17196=EDGE_CURVE ( 'NONE', #2064, #10678, #16662, .T. ) ;
#17197=CARTESIAN_POINT ( 'NONE',  ( -24.94770155647771048, 1.648570732456370536, 9.868708321403529382 ) ) ;
#17199=TOROIDAL_SURFACE ( 'NONE', #10372, 24.63401512838747820, 3.000000000000000888 ) ;
#17209=ORIENTED_EDGE ( 'NONE', *, *, #1596, .F. ) ;
#17242=ORIENTED_EDGE ( 'NONE', *, *, #16998, .F. ) ;
#17250=DIRECTION ( 'NONE',  ( 0.000000000000000000, 0.000000000000000000, 1.000000000000000000 ) ) ;
#17271=DIRECTION ( 'NONE',  ( 0.000000000000000000, 0.000000000000000000, 1.000000000000000000 ) ) ;
#17286=CARTESIAN_POINT ( 'NONE',  ( 0.000000000000000000, 0.000000000000000000, -55.00000000000000000 ) ) ;
#17290=CARTESIAN_POINT ( 'NONE',  ( 0.000000000000000000, 0.000000000000000000, 75.00000000000000000 ) ) ;
#17299=CARTESIAN_POINT ( 'NONE',  ( -22.85901762761804079, 2.624492169728419810, 9.672053823688761653 ) ) ;
#17303=CARTESIAN_POINT ( 'NONE',  ( -23.28342401362511183, 9.104969700446932990, 4.148060178146769417 ) ) ;
#17316=ORIENTED_EDGE ( 'NONE', *, *, #10754, .T. ) ;
#17321=AXIS2_PLACEMENT_3D ( 'NONE', #18060, #19626, #11089 ) ;
#17328=PLANE ( 'NONE',  #10984 ) ;
#17337=ORIENTED_EDGE ( 'NONE', *, *, #6998, .T. ) ;
#17384=VERTEX_POINT ( 'NONE', #12236 ) ;
#17391=AXIS2_PLACEMENT_3D ( 'NONE', #4221, #9200, #17752 ) ;
#17400=ADVANCED_FACE ( 'NONE', ( #17418 ), #14869, .T. ) ;
#17402=DIRECTION ( 'NONE',  ( 0.000000000000000000, 0.000000000000000000, -1.000000000000000000 ) ) ;
#17410=DIRECTION ( 'NONE',  ( 0.000000000000000000, 0.000000000000000000, 1.000000000000000000 ) ) ;
#17418=FACE_OUTER_BOUND ( 'NONE', #15730, .T. ) ;
#17419=CARTESIAN_POINT ( 'NONE',  ( -21.95791705875131683, 6.848931874401857023, 7.293650334809576030 ) ) ;
#17423=CARTESIAN_POINT ( 'NONE',  ( -23.05316956679390472, 9.673225031394522944, 2.619284265031635250 ) ) ;
#17434=AXIS2_PLACEMENT_3D ( 'NONE', #13792, #17271, #8839 ) ;
#17467=DIRECTION ( 'NONE',  ( 0.000000000000000000, 0.000000000000000000, 1.000000000000000000 ) ) ;
#17478=CARTESIAN_POINT ( 'NONE',  ( -23.00000000000008882, 0.000000000000000000, 75.00000000000000000 ) ) ;
#17479=EDGE_CURVE ( 'NONE', #8407, #20454, #2994, .T. ) ;
#17502=CARTESIAN_POINT ( 'NONE',  ( 0.000000000000000000, 0.000000000000000000, 75.00000000000000000 ) ) ;
#17512=VERTEX_POINT ( 'NONE', #10438 ) ;
#17530=CARTESIAN_POINT ( 'NONE',  ( 1.665334536937735820E-13, -23.00000000000006040, 69.99999999999998579 ) ) ;
#17539=DIRECTION ( 'NONE',  ( -1.000000000000000000, 0.000000000000000000, 0.000000000000000000 ) ) ;
#17546=ORIENTED_EDGE ( 'NONE', *, *, #14512, .F. ) ;
#17548=CARTESIAN_POINT ( 'NONE',  ( 2.465190328815661892E-29, 25.00000000000012790, 75.00000000000000000 ) ) ;
#17549=ORIENTED_EDGE ( 'NONE', *, *, #14990, .F. ) ;
#17580=EDGE_CURVE ( 'NONE', #12201, #4564, #12351, .T. ) ;
#17588=CARTESIAN_POINT ( 'NONE',  ( -19.80000000000007532, 0.000000000000000000, 78.50000000000000000 ) ) ;
#17601=EDGE_CURVE ( 'NONE', #9851, #6126, #526, .T. ) ;
#17615=DIRECTION ( 'NONE',  ( -1.000000000000000000, 0.000000000000000000, 0.000000000000000000 ) ) ;
#17619=EDGE_LOOP ( 'NONE', ( #4884, #5435, #2987, #17337, #8768, #17549 ) ) ;
#17636=CARTESIAN_POINT ( 'NONE',  ( -24.79104265374166260, -3.241215102701672457, -9.465926045374253306 ) ) ;
#17637=CARTESIAN_POINT ( 'NONE',  ( -22.96438540778823878, 1.321627609350921384, 9.917856572734910614 ) ) ;
#17648=CIRCLE ( 'NONE', #9785, 3.000000000000002665 ) ;
#17665=FACE_OUTER_BOUND ( 'NONE', #14711, .T. ) ;
#17666=DIRECTION ( 'NONE',  ( 0.000000000000000000, 0.000000000000000000, 1.000000000000000000 ) ) ;
#17682=CYLINDRICAL_SURFACE ( 'NONE', #20172, 17.50000000000007816 ) ;
#17698=DIRECTION ( 'NONE',  ( 1.000000000000000000, 0.000000000000000000, 0.000000000000000000 ) ) ;
#17710=AXIS2_PLACEMENT_3D ( 'NONE', #10397, #5203, #12086 ) ;
#17730=ORIENTED_EDGE ( 'NONE', *, *, #1150, .T. ) ;
#17732=ORIENTED_EDGE ( 'NONE', *, *, #2798, .F. ) ;
#17739=ORIENTED_EDGE ( 'NONE', *, *, #4471, .F. ) ;
#17746=CIRCLE ( 'NONE', #11632, 3.000000000000002665 ) ;
#17751=AXIS2_PLACEMENT_3D ( 'NONE', #197, #3560, #15617 ) ;
#17752=DIRECTION ( 'NONE',  ( -1.000000000000000000, 0.000000000000000000, 0.000000000000000000 ) ) ;
#17763=EDGE_LOOP ( 'NONE', ( #5484, #18862, #5152, #14529, #3376, #19412 ) ) ;
#17844=ORIENTED_EDGE ( 'NONE', *, *, #19866, .T. ) ;
#17864=EDGE_CURVE ( 'NONE', #10566, #18119, #10193, .T. ) ;
#17893=CARTESIAN_POINT ( 'NONE',  ( 0.000000000000000000, 0.000000000000000000, -77.51594804401857175 ) ) ;
#17894=PLANE ( 'NONE',  #8011 ) ;
#17900=VERTEX_POINT ( 'NONE', #12352 ) ;
#17936=CIRCLE ( 'NONE', #336, 23.00000000000008882 ) ;
#17940=DIRECTION ( 'NONE',  ( -1.000000000000000000, 0.000000000000000000, 0.000000000000000000 ) ) ;
#17951=ORIENTED_EDGE ( 'NONE', *, *, #19702, .F. ) ;
#17956=CARTESIAN_POINT ( 'NONE',  ( 0.000000000000000000, 0.000000000000000000, -69.99999999999998579 ) ) ;
#17957=ORIENTED_EDGE ( 'NONE', *, *, #19709, .F. ) ;
#17976=ORIENTED_EDGE ( 'NONE', *, *, #16436, .F. ) ;
#17981=ORIENTED_EDGE ( 'NONE', *, *, #6515, .F. ) ;
#17992=DIRECTION ( 'NONE',  ( -1.000000000000000000, 0.000000000000000000, 0.000000000000000000 ) ) ;
#18008=ORIENTED_EDGE ( 'NONE', *, *, #440, .F. ) ;
#18021=ORIENTED_EDGE ( 'NONE', *, *, #12996, .F. ) ;
#18028=CARTESIAN_POINT ( 'NONE',  ( 0.000000000000000000, 0.000000000000000000, 0.000000000000000000 ) ) ;
#18036=CARTESIAN_POINT ( 'NONE',  ( 4.814824860968089633E-30, 19.63401512838754215, -77.51594804401857175 ) ) ;
#18055=VERTEX_POINT ( 'NONE', #3783 ) ;
#18060=CARTESIAN_POINT ( 'NONE',  ( 1.665334536937735316E-13, -24.63401512838760610, -77.51594804401857175 ) ) ;
#18074=CARTESIAN_POINT ( 'NONE',  ( -20.86829502391188029, 9.671354583073858535, 2.626725457081121373 ) ) ;
#18082=EDGE_CURVE ( 'NONE', #2515, #14027, #10665, .T. ) ;
#18084=DIRECTION ( 'NONE',  ( -0.000000000000000000, 0.000000000000000000, -1.000000000000000000 ) ) ;
#18092=EDGE_CURVE ( 'NONE', #9851, #12391, #15480, .T. ) ;
#18104=CARTESIAN_POINT ( 'NONE',  ( -24.24581955882289819, 6.099808590248922080, -7.930829530152172069 ) ) ;
#18119=VERTEX_POINT ( 'NONE', #13003 ) ;
#18141=FILL_AREA_STYLE ('',( #2816 ) ) ;
#18150=CARTESIAN_POINT ( 'NONE',  ( 0.000000000000000000, 0.000000000000000000, -77.51594804401857175 ) ) ;
#18157=ADVANCED_FACE ( 'NONE', ( #6023 ), #21433, .F. ) ;
#18185=VERTEX_POINT ( 'NONE', #4552 ) ;
#18188=CARTESIAN_POINT ( 'NONE',  ( -23.70746030402021631, -7.943882500033654814, -6.109207967854218602 ) ) ;
#18199=( GEOMETRIC_REPRESENTATION_CONTEXT ( 3 ) GLOBAL_UNCERTAINTY_ASSIGNED_CONTEXT ( ( #3109 ) ) GLOBAL_UNIT_ASSIGNED_CONTEXT ( ( #15845, #12472, #15956 ) ) REPRESENTATION_CONTEXT ( 'NONE', 'WORKASPACE' ) );
#18223=CARTESIAN_POINT ( 'NONE',  ( -22.24611232821838058, -5.847058217106408939, -8.118985252087330906 ) ) ;
#18224=CARTESIAN_POINT ( 'NONE',  ( 0.000000000000000000, 0.000000000000000000, -60.00000000000000000 ) ) ;
#18288=ADVANCED_FACE ( 'NONE', ( #4608 ), #16113, .T. ) ;
#18289=CARTESIAN_POINT ( 'NONE',  ( -24.63401512838757768, 0.000000000000000000, 77.51594804401857175 ) ) ;
#18297=CARTESIAN_POINT ( 'NONE',  ( -24.30915884321608544, -5.843097688897257669, -8.121843009851255957 ) ) ;
#18320=DIRECTION ( 'NONE',  ( 0.000000000000000000, 0.000000000000000000, 1.000000000000000000 ) ) ;
#18351=LINE ( 'NONE', #19389, #10597 ) ;
#18358=( LENGTH_UNIT ( ) NAMED_UNIT ( * ) SI_UNIT ( .MILLI., .METRE. ) );
#18360=EDGE_CURVE ( 'NONE', #8526, #8590, #16219, .T. ) ;
#18365=EDGE_CURVE ( 'NONE', #14027, #2064, #12952, .T. ) ;
#18393=CIRCLE ( 'NONE', #13364, 23.00000000000008882 ) ;
#18406=CARTESIAN_POINT ( 'NONE',  ( -24.49471200173250907, -5.031606206670845793, -8.666454690105759084 ) ) ;
#18428=DIRECTION ( 'NONE',  ( -1.083936797661037871E-15, -1.000000000000000000, 0.000000000000000000 ) ) ;
#18430=DIRECTION ( 'NONE',  ( 1.000000000000000000, 0.000000000000000000, 0.000000000000000000 ) ) ;
#18435=VECTOR ( 'NONE', #14410, 1000.000000000000000 ) ;
#18441=CARTESIAN_POINT ( 'NONE',  ( -20.83650439078820682, -9.738852918555068072, -2.294278442558280506 ) ) ;
#18450=CARTESIAN_POINT ( 'NONE',  ( -2.465190328815661892E-29, -25.00000000000012790, 75.00000000000000000 ) ) ;
#18467=DIRECTION ( 'NONE',  ( -1.000000000000000000, 0.000000000000000000, 0.000000000000000000 ) ) ;
#18468=DIRECTION ( 'NONE',  ( 1.000000000000000000, -1.083936797661038068E-15, 0.000000000000000000 ) ) ;
#18479=EDGE_CURVE ( 'NONE', #20995, #19105, #9442, .T. ) ;
#18484=TOROIDAL_SURFACE ( 'NONE', #7029, 24.63401512838747820, 3.000000000000000888 ) ;
#18489=ORIENTED_EDGE ( 'NONE', *, *, #4731, .T. ) ;
#18519=CARTESIAN_POINT ( 'NONE',  ( -23.45299820629349696, -8.666215563591268989, 5.031560091074801733 ) ) ;
#18536=ORIENTED_EDGE ( 'NONE', *, *, #4685, .T. ) ;
#18540=CARTESIAN_POINT ( 'NONE',  ( 0.000000000000000000, 0.000000000000000000, 75.00000000000000000 ) ) ;
#18554=CIRCLE ( 'NONE', #5610, 23.00000000000008882 ) ;
#18557=DIRECTION ( 'NONE',  ( 0.000000000000000000, -1.000000000000000000, 0.000000000000000000 ) ) ;
#18574=EDGE_CURVE ( 'NONE', #17512, #9712, #12736, .T. ) ;
#18581=CARTESIAN_POINT ( 'NONE',  ( 0.000000000000000000, 0.000000000000000000, -60.00000000000000000 ) ) ;
#18596=DIRECTION ( 'NONE',  ( -1.000000000000000000, 0.000000000000000000, 0.000000000000000000 ) ) ;
#18621=CARTESIAN_POINT ( 'NONE',  ( 0.000000000000000000, 0.000000000000000000, -77.51594804401857175 ) ) ;
#18628=VERTEX_POINT ( 'NONE', #19689 ) ;
#18649=CARTESIAN_POINT ( 'NONE',  ( -23.00000000000000000, 0.000000000000000000, 69.99999999999998579 ) ) ;
#18655=DIRECTION ( 'NONE',  ( -0.000000000000000000, 0.000000000000000000, -1.000000000000000000 ) ) ;
#18699=VERTEX_POINT ( 'NONE', #5054 ) ;
#18701=ORIENTED_EDGE ( 'NONE', *, *, #12124, .F. ) ;
#18733=EDGE_LOOP ( 'NONE', ( #12273, #11912, #14243, #2025, #14544, #1487 ) ) ;
#18737=DIRECTION ( 'NONE',  ( -0.000000000000000000, 0.000000000000000000, -1.000000000000000000 ) ) ;
#18752=ORIENTED_EDGE ( 'NONE', *, *, #16821, .F. ) ;
#18757=CIRCLE ( 'NONE', #12998, 17.50000000000007816 ) ;
#18770=CARTESIAN_POINT ( 'NONE',  ( 1.232595164407830946E-29, -17.50000000000007105, -30.00000000000000000 ) ) ;
#18795=LINE ( 'NONE', #10245, #11279 ) ;
#18812=LINE ( 'NONE', #3383, #6206 ) ;
#18819=ORIENTED_EDGE ( 'NONE', *, *, #8587, .F. ) ;
#18839=ADVANCED_FACE ( 'NONE', ( #22172 ), #13630, .T. ) ;
#18862=ORIENTED_EDGE ( 'NONE', *, *, #14770, .T. ) ;
#18865=CARTESIAN_POINT ( 'NONE',  ( -24.63401512838757768, 0.000000000000000000, 77.51594804401857175 ) ) ;
#18874=DIRECTION ( 'NONE',  ( -1.000000000000000000, 0.000000000000000000, 0.000000000000000000 ) ) ;
#18876=DIRECTION ( 'NONE',  ( 0.000000000000000000, 0.000000000000000000, -1.000000000000000000 ) ) ;
#18879=EDGE_CURVE ( 'NONE', #14742, #8296, #6526, .T. ) ;
#18904=CYLINDRICAL_SURFACE ( 'NONE', #5579, 23.00000000000008882 ) ;
#18921=CARTESIAN_POINT ( 'NONE',  ( -17.50000000000000711, 0.000000000000000000, -30.00000000000000000 ) ) ;
#18949=ORIENTED_EDGE ( 'NONE', *, *, #16032, .F. ) ;
#18952=ORIENTED_EDGE ( 'NONE', *, *, #4317, .F. ) ;
#18986=CARTESIAN_POINT ( 'NONE',  ( -23.13355025916758834, 9.482198088197261399, 3.242749661402037020 ) ) ;
#18989=TOROIDAL_SURFACE ( 'NONE', #13979, 24.63401512838747820, 3.000000000000000888 ) ;
#19004=ADVANCED_FACE ( 'NONE', ( #2019 ), #2936, .F. ) ;
#19018=ORIENTED_EDGE ( 'NONE', *, *, #983, .F. ) ;
#19025=CARTESIAN_POINT ( 'NONE',  ( -25.00000000000010303, 0.000000000000000000, 75.00000000000000000 ) ) ;
#19076=VERTEX_POINT ( 'NONE', #3481 ) ;
#19087=CARTESIAN_POINT ( 'NONE',  ( 0.000000000000000000, 0.000000000000000000, 77.51594804401857175 ) ) ;
#19088=CARTESIAN_POINT ( 'NONE',  ( -22.56563535238560902, 4.458514667912840679, 8.957021455394174936 ) ) ;
#19092=CARTESIAN_POINT ( 'NONE',  ( -22.94128848581996039, 9.935662058461005586, -1.312836635664774043 ) ) ;
#19105=VERTEX_POINT ( 'NONE', #1794 ) ;
#19118=CARTESIAN_POINT ( 'NONE',  ( 0.000000000000000000, 0.000000000000000000, 77.51594804401857175 ) ) ;
#19140=AXIS2_PLACEMENT_3D ( 'NONE', #21575, #6163, #19886 ) ;
#19147=DIRECTION ( 'NONE',  ( -0.000000000000000000, 0.000000000000000000, -1.000000000000000000 ) ) ;
#19150=CARTESIAN_POINT ( 'NONE',  ( -25.00000000000013500, 1.972152263052529514E-28, 0.000000000000000000 ) ) ;
#19162=ADVANCED_FACE ( 'NONE', ( #3813 ), #11233, .F. ) ;
#19168=ORIENTED_EDGE ( 'NONE', *, *, #1211, .F. ) ;
#19180=CARTESIAN_POINT ( 'NONE',  ( 0.000000000000000000, 0.000000000000000000, -77.51594804401857175 ) ) ;
#19184=ORIENTED_EDGE ( 'NONE', *, *, #10506, .F. ) ;
#19200=ORIENTED_EDGE ( 'NONE', *, *, #8422, .F. ) ;
#19220=ORIENTED_EDGE ( 'NONE', *, *, #16998, .T. ) ;
#19261=AXIS2_PLACEMENT_3D ( 'NONE', #3950, #3841, #10722 ) ;
#19286=FACE_OUTER_BOUND ( 'NONE', #13244, .T. ) ;
#19311=ORIENTED_EDGE ( 'NONE', *, *, #3598, .T. ) ;
#19320=EDGE_CURVE ( 'NONE', #18628, #8679, #448, .T. ) ;
#19358=CARTESIAN_POINT ( 'NONE',  ( 0.000000000000000000, 0.000000000000000000, -24.99999999999999645 ) ) ;
#19389=CARTESIAN_POINT ( 'NONE',  ( 0.000000000000000000, -23.00000000000006040, -75.00000000000000000 ) ) ;
#19412=ORIENTED_EDGE ( 'NONE', *, *, #20644, .F. ) ;
#19445=DIRECTION ( 'NONE',  ( -1.000000000000000000, 0.000000000000000000, 0.000000000000000000 ) ) ;
#19452=ORIENTED_EDGE ( 'NONE', *, *, #6515, .T. ) ;
#19496=LINE ( 'NONE', #11072, #14557 ) ;
#19515=DIRECTION ( 'NONE',  ( 0.000000000000000000, 0.000000000000000000, -1.000000000000000000 ) ) ;
#19516=EDGE_CURVE ( 'NONE', #17512, #18185, #16094, .T. ) ;
#19538=ORIENTED_EDGE ( 'NONE', *, *, #19894, .F. ) ;
#19555=CARTESIAN_POINT ( 'NONE',  ( 0.000000000000000000, 23.00000000000006040, 75.00000000000000000 ) ) ;
#19558=DIRECTION ( 'NONE',  ( 0.000000000000000000, 1.000000000000000000, 0.000000000000000000 ) ) ;
#19559=CIRCLE ( 'NONE', #21708, 19.80000000000007887 ) ;
#19560=CARTESIAN_POINT ( 'NONE',  ( 0.000000000000000000, 22.63401512838754570, -77.51594804401857175 ) ) ;
#19580=DIRECTION ( 'NONE',  ( -2.162300680179986877E-16, -1.000000000000000000, 0.000000000000000000 ) ) ;
#19581=VERTEX_POINT ( 'NONE', #7650 ) ;
#19590=EDGE_CURVE ( 'NONE', #9712, #15083, #4386, .T. ) ;
#19609=CARTESIAN_POINT ( 'NONE',  ( 0.000000000000000000, 23.00000000000006040, -60.00000000000000000 ) ) ;
#19626=DIRECTION ( 'NONE',  ( 1.000000000000000000, 6.982962677686272233E-15, 0.000000000000000000 ) ) ;
#19641=PRESENTATION_STYLE_ASSIGNMENT (( #12795 ) ) ;
#19659=CARTESIAN_POINT ( 'NONE',  ( 1.317067778529001989E-13, -19.63401512838754215, 77.51594804401857175 ) ) ;
#19667=CARTESIAN_POINT ( 'NONE',  ( -22.97082590106532507, -1.326754249648130157, -9.933407853828526868 ) ) ;
#19668=CARTESIAN_POINT ( 'NONE',  ( 1.665334536937735820E-13, -23.00000000000006040, -69.99999999999998579 ) ) ;
#19678=ADVANCED_FACE ( 'NONE', ( #11027 ), #17894, .T. ) ;
#19689=CARTESIAN_POINT ( 'NONE',  ( 1.232595164407830946E-29, -17.50000000000007105, -24.99999999999999645 ) ) ;
#19702=EDGE_CURVE ( 'NONE', #14415, #12893, #21356, .T. ) ;
#19709=EDGE_CURVE ( 'NONE', #9941, #10887, #16281, .T. ) ;
#19710=AXIS2_PLACEMENT_3D ( 'NONE', #4131, #7961, #4455 ) ;
#19713=ORIENTED_EDGE ( 'NONE', *, *, #17601, .T. ) ;
#19715=ADVANCED_FACE ( 'NONE', ( #16309 ), #14845, .T. ) ;
#19727=ORIENTED_EDGE ( 'NONE', *, *, #14990, .T. ) ;
#19732=CYLINDRICAL_SURFACE ( 'NONE', #7971, 21.00000000000008171 ) ;
#19744=CARTESIAN_POINT ( 'NONE',  ( -22.91305488956320957, -9.999595782860119186, -0.6663400851647119927 ) ) ;
#19752=PLANE ( 'NONE',  #22016 ) ;
#19766=DIRECTION ( 'NONE',  ( 0.000000000000000000, 0.000000000000000000, -1.000000000000000000 ) ) ;
#19770=CARTESIAN_POINT ( 'NONE',  ( -23.45461921731179800, 8.654954236178731719, -5.019855114128365159 ) ) ;
#19772=CARTESIAN_POINT ( 'NONE',  ( -25.00000000000000000, -1.002884296170500229E-19, 10.00000000000000000 ) ) ;
#19821=AXIS2_PLACEMENT_3D ( 'NONE', #6630, #13500, #8657 ) ;
#19849=CARTESIAN_POINT ( 'NONE',  ( -23.84416809906481305, -7.516854498463030332, 6.603279950623392125 ) ) ;
#19850=CARTESIAN_POINT ( 'NONE',  ( -21.58811430103374818, 7.943727580301767510, -6.108684005820687268 ) ) ;
#19853=CIRCLE ( 'NONE', #15912, 23.00000000000008882 ) ;
#19859=CARTESIAN_POINT ( 'NONE',  ( 0.000000000000000000, 0.000000000000000000, 69.99999999999998579 ) ) ;
#19862=ORIENTED_EDGE ( 'NONE', *, *, #5142, .F. ) ;
#19866=EDGE_CURVE ( 'NONE', #3746, #15108, #11240, .T. ) ;
#19876=TOROIDAL_SURFACE ( 'NONE', #1909, 22.63401512838748175, 3.000000000000002665 ) ;
#19877=CIRCLE ( 'NONE', #5869, 3.000000000000002665 ) ;
#19880=CARTESIAN_POINT ( 'NONE',  ( -24.86519201702800430, 2.611873406124941788, -9.658447518498306295 ) ) ;
#19885=CARTESIAN_POINT ( 'NONE',  ( -22.57082077310269952, -4.464701546683219391, -8.971916582499627424 ) ) ;
#19886=DIRECTION ( 'NONE',  ( -1.000000000000000000, 0.000000000000000000, 0.000000000000000000 ) ) ;
#19894=EDGE_CURVE ( 'NONE', #1644, #19076, #1548, .T. ) ;
#19910=DIRECTION ( 'NONE',  ( -1.000000000000000000, 0.000000000000000000, 0.000000000000000000 ) ) ;
#19917=ADVANCED_FACE ( 'NONE', ( #9561 ), #998, .F. ) ;
#19952=DIRECTION ( 'NONE',  ( -1.000000000000000000, 0.000000000000000000, 0.000000000000000000 ) ) ;
#19953=EDGE_CURVE ( 'NONE', #6126, #2334, #21242, .T. ) ;
#19956=DIRECTION ( 'NONE',  ( 0.000000000000000000, 1.000000000000000000, -0.000000000000000000 ) ) ;
#19965=CARTESIAN_POINT ( 'NONE',  ( -24.60379713026238235, -4.442902817157290407, 8.964804537911287952 ) ) ;
#19983=ORIENTED_EDGE ( 'NONE', *, *, #6596, .T. ) ;
#19995=CARTESIAN_POINT ( 'NONE',  ( -19.63401512838757057, 1.925929944387226885E-29, -77.51594804401857175 ) ) ;
#20021=DIRECTION ( 'NONE',  ( 4.845403715540905824E-30, -6.938893903907257960E-16, 1.000000000000000000 ) ) ;
#20029=SURFACE_STYLE_FILL_AREA ( #18141 ) ;
#20073=CARTESIAN_POINT ( 'NONE',  ( -23.18452556481357618, -9.353925523610076453, -3.551024142333974787 ) ) ;
#20081=CARTESIAN_POINT ( 'NONE',  ( 0.000000000000000000, 0.000000000000000000, -75.00000000000000000 ) ) ;
#20103=EDGE_CURVE ( 'NONE', #8392, #10586, #7044, .T. ) ;
#20105=CARTESIAN_POINT ( 'NONE',  ( 0.000000000000000000, 21.80000000000006111, 78.50000000000000000 ) ) ;
#20126=CARTESIAN_POINT ( 'NONE',  ( -23.00000000000000000, 0.000000000000000000, -55.00000000000000000 ) ) ;
#20172=AXIS2_PLACEMENT_3D ( 'NONE', #19358, #14091, #20931 ) ;
#20174=VERTEX_POINT ( 'NONE', #15711 ) ;
#20178=CARTESIAN_POINT ( 'NONE',  ( 0.000000000000000000, 0.000000000000000000, 78.50000000000000000 ) ) ;
#20207=AXIS2_PLACEMENT_3D ( 'NONE', #12767, #5775, #20859 ) ;
#20210=CARTESIAN_POINT ( 'NONE',  ( -1.232595164407830946E-29, 17.50000000000007105, -60.00000000000000000 ) ) ;
#20223=CARTESIAN_POINT ( 'NONE',  ( 1.526556658859590748E-13, -21.00000000000006395, 75.00000000000000000 ) ) ;
#20226=AXIS2_PLACEMENT_3D ( 'NONE', #14730, #21682, #16632 ) ;
#20236=VECTOR ( 'NONE', #13851, 1000.000000000000000 ) ;
#20250=EDGE_LOOP ( 'NONE', ( #16100, #19452, #19862, #4456 ) ) ;
#20254=DIRECTION ( 'NONE',  ( -1.000000000000000000, 0.000000000000000000, 0.000000000000000000 ) ) ;
#20257=CIRCLE ( 'NONE', #1228, 3.000000000000002665 ) ;
#20274=AXIS2_PLACEMENT_3D ( 'NONE', #21712, #13284, #14351 ) ;
#20307=DIRECTION ( 'NONE',  ( 1.000000000000000000, 0.000000000000000000, 0.000000000000000000 ) ) ;
#20309=CIRCLE ( 'NONE', #10630, 3.000000000000002665 ) ;
#20313=DIRECTION ( 'NONE',  ( 0.000000000000000000, 1.000000000000000000, -0.000000000000000000 ) ) ;
#20315=FACE_OUTER_BOUND ( 'NONE', #16570, .T. ) ;
#20327=MECHANICAL_DESIGN_GEOMETRIC_PRESENTATION_REPRESENTATION('',(#14611),#16399);
#20336=ORIENTED_EDGE ( 'NONE', *, *, #18574, .T. ) ;
#20344=CIRCLE ( 'NONE', #950, 23.00000000000008882 ) ;
#20352=CARTESIAN_POINT ( 'NONE',  ( -23.00000000000000000, -1.421401133463427911E-20, 10.00000000000000000 ) ) ;
#20354=CARTESIAN_POINT ( 'NONE',  ( 2.465190328815661892E-29, 25.00000000000012790, 75.00000000000000000 ) ) ;
#20364=VERTEX_POINT ( 'NONE', #1442 ) ;
#20404=ORIENTED_EDGE ( 'NONE', *, *, #19866, .F. ) ;
#20429=DIRECTION ( 'NONE',  ( -0.000000000000000000, 0.000000000000000000, -1.000000000000000000 ) ) ;
#20438=CARTESIAN_POINT ( 'NONE',  ( -1.232595164407830946E-29, 17.50000000000007105, -55.00000000000000000 ) ) ;
#20452=PLANE ( 'NONE',  #20554 ) ;
#20453=EDGE_LOOP ( 'NONE', ( #21958, #21874, #837, #17957 ) ) ;
#20454=VERTEX_POINT ( 'NONE', #20105 ) ;
#20475=ORIENTED_EDGE ( 'NONE', *, *, #19953, .F. ) ;
#20495=DIRECTION ( 'NONE',  ( 1.000000000000000000, 6.982962677686272233E-15, 0.000000000000000000 ) ) ;
#20536=VECTOR ( 'NONE', #3712, 1000.000000000000000 ) ;
#20538=DIRECTION ( 'NONE',  ( 1.000000000000000000, 0.000000000000000000, 0.000000000000000000 ) ) ;
#20547=CARTESIAN_POINT ( 'NONE',  ( 0.000000000000000000, 19.80000000000006111, 78.50000000000000000 ) ) ;
#20548=DIRECTION ( 'NONE',  ( -0.000000000000000000, 0.000000000000000000, -1.000000000000000000 ) ) ;
#20550=CARTESIAN_POINT ( 'NONE',  ( 2.465190328815661892E-29, 24.63401512838760610, -77.51594804401857175 ) ) ;
#20551=CARTESIAN_POINT ( 'NONE',  ( -22.85901844618171097, -2.626155446365975976, 9.672066817478860656 ) ) ;
#20554=AXIS2_PLACEMENT_3D ( 'NONE', #5041, #3350, #2115 ) ;
#20558=ORIENTED_EDGE ( 'NONE', *, *, #13692, .F. ) ;
#20562=ORIENTED_EDGE ( 'NONE', *, *, #5532, .T. ) ;
#20564=CARTESIAN_POINT ( 'NONE',  ( 0.000000000000000000, 0.000000000000000000, -30.00000000000000000 ) ) ;
#20565=ORIENTED_EDGE ( 'NONE', *, *, #18365, .F. ) ;
#20570=AXIS2_PLACEMENT_3D ( 'NONE', #6077, #2478, #19910 ) ;
#20587=ORIENTED_EDGE ( 'NONE', *, *, #15067, .F. ) ;
#20594=PLANE ( 'NONE',  #5853 ) ;
#20597=AXIS2_PLACEMENT_3D ( 'NONE', #15297, #11566, #15182 ) ;
#20618=AXIS2_PLACEMENT_3D ( 'NONE', #13484, #18876, #13710 ) ;
#20619=PLANE ( 'NONE',  #17710 ) ;
#20620=ADVANCED_BREP_SHAPE_REPRESENTATION ( '', ( #6837, #6677 ), #2013 ) ;
#20644=EDGE_CURVE ( 'NONE', #11119, #13087, #3333, .T. ) ;
#20651=ORIENTED_EDGE ( 'NONE', *, *, #6499, .T. ) ;
#20662=DIRECTION ( 'NONE',  ( -1.000000000000000000, -6.982962677686272233E-15, 0.000000000000000000 ) ) ;
#20663=CARTESIAN_POINT ( 'NONE',  ( -21.31134010702326975, 8.651877420333450530, 5.025164282198873344 ) ) ;
#20667=CARTESIAN_POINT ( 'NONE',  ( -23.45512409874873683, 8.653582270224204009, 5.022182943822000922 ) ) ;
#20723=CARTESIAN_POINT ( 'NONE',  ( 0.000000000000000000, 0.000000000000000000, 75.00000000000000000 ) ) ;
#20724=ADVANCED_FACE ( 'NONE', ( #10852 ), #12331, .F. ) ;
#20771=DIRECTION ( 'NONE',  ( 1.000000000000000000, 6.982962677686272233E-15, 0.000000000000000000 ) ) ;
#20789=CARTESIAN_POINT ( 'NONE',  ( 0.000000000000000000, 0.000000000000000000, -30.00000000000000000 ) ) ;
#20800=LINE ( 'NONE', #21024, #20236 ) ;
#20803=DIRECTION ( 'NONE',  ( -0.000000000000000000, 0.000000000000000000, -1.000000000000000000 ) ) ;
#20819=CYLINDRICAL_SURFACE ( 'NONE', #16299, 17.50000000000007816 ) ;
#20859=DIRECTION ( 'NONE',  ( 1.000000000000000000, 0.000000000000000000, 0.000000000000000000 ) ) ;
#20869=ORIENTED_EDGE ( 'NONE', *, *, #13238, .T. ) ;
#20872=DIRECTION ( 'NONE',  ( 0.000000000000000000, 0.000000000000000000, -1.000000000000000000 ) ) ;
#20886=CARTESIAN_POINT ( 'NONE',  ( 2.465190328815661892E-29, 25.00000000000012790, -75.00000000000000000 ) ) ;
#20894=ORIENTED_EDGE ( 'NONE', *, *, #17864, .T. ) ;
#20915=CARTESIAN_POINT ( 'NONE',  ( 0.000000000000000000, 0.000000000000000000, 77.51594804401857175 ) ) ;
#20926=AXIS2_PLACEMENT_3D ( 'NONE', #20915, #17666, #7211 ) ;
#20931=DIRECTION ( 'NONE',  ( -1.000000000000000000, 0.000000000000000000, 0.000000000000000000 ) ) ;
#20954=DIRECTION ( 'NONE',  ( -1.000000000000000000, 0.000000000000000000, 0.000000000000000000 ) ) ;
#20959=ADVANCED_FACE ( 'NONE', ( #2403 ), #7397, .T. ) ;
#20964=ORIENTED_EDGE ( 'NONE', *, *, #2109, .F. ) ;
#20986=CARTESIAN_POINT ( 'NONE',  ( 0.000000000000000000, 0.000000000000000000, -55.00000000000000000 ) ) ;
#20995=VERTEX_POINT ( 'NONE', #14250 ) ;
#20998=CARTESIAN_POINT ( 'NONE',  ( -25.00000000000013500, -0.6682719527943432603, -10.00000000000000178 ) ) ;
#21005=DIRECTION ( 'NONE',  ( -0.000000000000000000, 0.000000000000000000, -1.000000000000000000 ) ) ;
#21016=ORIENTED_EDGE ( 'NONE', *, *, #6596, .F. ) ;
#21024=CARTESIAN_POINT ( 'NONE',  ( -17.50000000000007816, 0.000000000000000000, -55.00000000000000000 ) ) ;
#21076=EDGE_LOOP ( 'NONE', ( #179, #10918, #20558, #2613 ) ) ;
#21077=DIRECTION ( 'NONE',  ( 0.000000000000000000, 0.000000000000000000, -1.000000000000000000 ) ) ;
#21088=ORIENTED_EDGE ( 'NONE', *, *, #2109, .T. ) ;
#21098=DIRECTION ( 'NONE',  ( -0.000000000000000000, 0.000000000000000000, -1.000000000000000000 ) ) ;
#21103=ORIENTED_EDGE ( 'NONE', *, *, #8010, .T. ) ;
#21107=CARTESIAN_POINT ( 'NONE',  ( -22.03299105905330535, 6.604150919132904640, -7.515967719178155981 ) ) ;
#21135=DIRECTION ( 'NONE',  ( 0.000000000000000000, 0.000000000000000000, -1.000000000000000000 ) ) ;
#21141=EDGE_LOOP ( 'NONE', ( #15963, #11315, #12691, #15157, #19168, #18752 ) ) ;
#21148=CIRCLE ( 'NONE', #19710, 23.00000000000008882 ) ;
#21170=FACE_OUTER_BOUND ( 'NONE', #1801, .T. ) ;
#21183=FACE_OUTER_BOUND ( 'NONE', #5480, .T. ) ;
#21213=CARTESIAN_POINT ( 'NONE',  ( -22.56530582151367170, 4.460126506072113806, -8.956185171266239919 ) ) ;
#21216=DIRECTION ( 'NONE',  ( -1.000000000000000000, 0.000000000000000000, 0.000000000000000000 ) ) ;
#21228=CARTESIAN_POINT ( 'NONE',  ( 1.317067778529001989E-13, -19.63401512838754215, -77.51594804401857175 ) ) ;
#21241=CARTESIAN_POINT ( 'NONE',  ( 0.000000000000000000, 21.00000000000006395, 75.00000000000000000 ) ) ;
#21242=LINE ( 'NONE', #5834, #1190 ) ;
#21262=CARTESIAN_POINT ( 'NONE',  ( 1.526556658859590748E-13, -21.00000000000006395, 75.00000000000000000 ) ) ;
#21268=VECTOR ( 'NONE', #20021, 1000.000000000000000 ) ;
#21298=EDGE_LOOP ( 'NONE', ( #20587, #1914, #4519, #16716 ) ) ;
#21299=CIRCLE ( 'NONE', #8023, 3.000000000000002665 ) ;
#21314=ORIENTED_EDGE ( 'NONE', *, *, #1150, .F. ) ;
#21354=DIRECTION ( 'NONE',  ( -1.000000000000000000, 0.000000000000000000, 0.000000000000000000 ) ) ;
#21355=AXIS2_PLACEMENT_3D ( 'NONE', #15374, #13678, #17056 ) ;
#21356=LINE ( 'NONE', #2457, #9820 ) ;
#21373=EDGE_CURVE ( 'NONE', #3236, #1365, #20309, .T. ) ;
#21394=DIRECTION ( 'NONE',  ( -4.408728476930457445E-15, 1.000000000000000000, 0.000000000000000000 ) ) ;
#21400=AXIS2_PLACEMENT_3D ( 'NONE', #478, #19147, #3726 ) ;
#21415=EDGE_LOOP ( 'NONE', ( #7499, #10257, #7746, #8776, #14610, #16981 ) ) ;
#21420=AXIS2_PLACEMENT_3D ( 'NONE', #4122, #10675, #11003 ) ;
#21433=CYLINDRICAL_SURFACE ( 'NONE', #108, 17.50000000000007816 ) ;
#21444=ORIENTED_EDGE ( 'NONE', *, *, #12643, .F. ) ;
#21450=CARTESIAN_POINT ( 'NONE',  ( -25.00000000000013500, 1.972152263052529514E-28, 0.000000000000000000 ) ) ;
#21463=CARTESIAN_POINT ( 'NONE',  ( 0.000000000000000000, -23.00000000000006040, -75.00000000000000000 ) ) ;
#21479=ADVANCED_FACE ( 'NONE', ( #145 ), #15565, .T. ) ;
#21509=ORIENTED_EDGE ( 'NONE', *, *, #17580, .F. ) ;
#21527=CARTESIAN_POINT ( 'NONE',  ( -23.00000000000000000, 0.000000000000000000, -69.99999999999998579 ) ) ;
#21538=DIRECTION ( 'NONE',  ( 0.000000000000000000, 0.000000000000000000, -1.000000000000000000 ) ) ;
#21539=CARTESIAN_POINT ( 'NONE',  ( -21.30892042260266095, 8.664836834455229564, -5.033828640834366652 ) ) ;
#21567=CARTESIAN_POINT ( 'NONE',  ( -23.51670878402428144, 8.485352115581564547, -5.301345601592732493 ) ) ;
#21575=CARTESIAN_POINT ( 'NONE',  ( 0.000000000000000000, 0.000000000000000000, 75.00000000000000000 ) ) ;
#21584=CARTESIAN_POINT ( 'NONE',  ( 0.000000000000000000, 0.000000000000000000, -77.51594804401857175 ) ) ;
#21602=EDGE_CURVE ( 'NONE', #10678, #9167, #4494, .T. ) ;
#21616=AXIS2_PLACEMENT_3D ( 'NONE', #13142, #11341, #11554 ) ;
#21628=DIRECTION ( 'NONE',  ( -1.000000000000000000, -6.982962677686272233E-15, 0.000000000000000000 ) ) ;
#21639=VECTOR ( 'NONE', #21135, 1000.000000000000000 ) ;
#21649=VERTEX_POINT ( 'NONE', #1724 ) ;
#21652=CARTESIAN_POINT ( 'NONE',  ( -23.05250587634771620, -9.674800950679635747, 2.613507269777442410 ) ) ;
#21671=CARTESIAN_POINT ( 'NONE',  ( -1.232595164407830946E-29, 17.50000000000007105, -55.00000000000000000 ) ) ;
#21678=AXIS2_PLACEMENT_3D ( 'NONE', #13708, #20771, #8868 ) ;
#21682=DIRECTION ( 'NONE',  ( -0.000000000000000000, 0.000000000000000000, -1.000000000000000000 ) ) ;
#21687=CARTESIAN_POINT ( 'NONE',  ( -21.95785083786292802, -6.849083017255801487, -7.293401492409205211 ) ) ;
#21696=AXIS2_PLACEMENT_3D ( 'NONE', #5915, #16170, #2316 ) ;
#21708=AXIS2_PLACEMENT_3D ( 'NONE', #5769, #21077, #17940 ) ;
#21712=CARTESIAN_POINT ( 'NONE',  ( 0.000000000000000000, 0.000000000000000000, 77.51594804401857175 ) ) ;
#21725=VECTOR ( 'NONE', #11710, 1000.000000000000000 ) ;
#21733=ORIENTED_EDGE ( 'NONE', *, *, #2519, .F. ) ;
#21754=CARTESIAN_POINT ( 'NONE',  ( 0.000000000000000000, 0.000000000000000000, -24.99999999999999645 ) ) ;
#21766=CARTESIAN_POINT ( 'NONE',  ( -24.04509347396444241, -6.847624739850214581, -7.294798726659911914 ) ) ;
#21778=AXIS2_PLACEMENT_3D ( 'NONE', #14537, #18320, #18430 ) ;
#21796=CARTESIAN_POINT ( 'NONE',  ( -25.00000000000013500, 0.3339166901145541044, -10.00000000000000000 ) ) ;
#21801=CARTESIAN_POINT ( 'NONE',  ( -22.38166440881320440, -5.304594382025126897, 8.483353619577671978 ) ) ;
#21835=VERTEX_POINT ( 'NONE', #3399 ) ;
#21848=CIRCLE ( 'NONE', #1737, 3.000000000000002665 ) ;
#21868=AXIS2_PLACEMENT_3D ( 'NONE', #21450, #11012, #9325 ) ;
#21874=ORIENTED_EDGE ( 'NONE', *, *, #21928, .F. ) ;
#21877=CARTESIAN_POINT ( 'NONE',  ( 0.000000000000000000, 0.000000000000000000, -24.99999999999999645 ) ) ;
#21911=CARTESIAN_POINT ( 'NONE',  ( -20.83653394098313427, -9.738788406788492225, 2.294410813807128413 ) ) ;
#21919=ORIENTED_EDGE ( 'NONE', *, *, #16995, .F. ) ;
#21921=DIRECTION ( 'NONE',  ( 1.401298464324817071E-45, 6.938893903907257960E-16, -1.000000000000000000 ) ) ;
#21928=EDGE_CURVE ( 'NONE', #15746, #12201, #16752, .T. ) ;
#21958=ORIENTED_EDGE ( 'NONE', *, *, #1722, .F. ) ;
#21985=ORIENTED_EDGE ( 'NONE', *, *, #1596, .T. ) ;
#21989=DIRECTION ( 'NONE',  ( 0.000000000000000000, 0.000000000000000000, 1.000000000000000000 ) ) ;
#22008=CARTESIAN_POINT ( 'NONE',  ( 0.000000000000000000, 21.00000000000006040, -69.99999999999998579 ) ) ;
#22016=AXIS2_PLACEMENT_3D ( 'NONE', #20081, #13013, #6139 ) ;
#22017=EDGE_CURVE ( 'NONE', #17384, #16873, #9929, .T. ) ;
#22027=CARTESIAN_POINT ( 'NONE',  ( -21.58840139808157232, -7.942961002574626228, 6.109722015442944354 ) ) ;
#22039=DIRECTION ( 'NONE',  ( 0.000000000000000000, 0.000000000000000000, 1.000000000000000000 ) ) ;
#22040=CIRCLE ( 'NONE', #2625, 19.63401512838747820 ) ;
#22048=EDGE_CURVE ( 'NONE', #4211, #17072, #13885, .T. ) ;
#22071=ADVANCED_FACE ( 'NONE', ( #13996 ), #5414, .F. ) ;
#22072=DIRECTION ( 'NONE',  ( 0.000000000000000000, 0.000000000000000000, -1.000000000000000000 ) ) ;
#22144=CIRCLE ( 'NONE', #12089, 3.000000000000002665 ) ;
#22145=DIRECTION ( 'NONE',  ( 0.000000000000000000, 0.000000000000000000, -1.000000000000000000 ) ) ;
#22156=ORIENTED_EDGE ( 'NONE', *, *, #13389, .T. ) ;
#22168=DIRECTION ( 'NONE',  ( 1.000000000000000000, 6.982962677686272233E-15, 0.000000000000000000 ) ) ;
#22172=FACE_OUTER_BOUND ( 'NONE', #6857, .T. ) ;
#22184=EDGE_CURVE ( 'NONE', #3468, #15083, #14763, .T. ) ;
#22191=EDGE_CURVE ( 'NONE', #12695, #21649, #10280, .T. ) ;
#22221=DIRECTION ( 'NONE',  ( -1.000000000000000000, 0.000000000000000000, 0.000000000000000000 ) ) ;
#22231=ORIENTED_EDGE ( 'NONE', *, *, #18082, .T. ) ;
#22235=AXIS2_PLACEMENT_3D ( 'NONE', #17071, #13468, #20307 ) ;
#22252=CARTESIAN_POINT ( 'NONE',  ( -20.87413353426600438, -9.658245891971773744, 2.612681058926761946 ) ) ;
ENDSEC;
END-ISO-10303-21;
